ISO-10303-21;
HEADER;
FILE_DESCRIPTION (('STEP AP214'),
    '1' );
FILE_NAME ('Hydraulic Index Locking Pin.step',
    '2026-10-07T11:37:37',
    ( '' ),
    ( '' ),
    'SwSTEP 2.0',
    'SolidWorks 2020',
    '' );
FILE_SCHEMA (( 'AUTOMOTIVE_DESIGN' ));
ENDSEC;

DATA;
#80=ADVANCED_FACE ( 'NONE', ( #30759 ), #10313, .F. ) ;
#99=CARTESIAN_POINT ( 'NONE',  ( 23.49611623194277499, 85.45756874832173366, 299.1102940853953100 ) ) ;
#116=DIRECTION ( 'NONE',  ( 0.000000000000000000, 0.000000000000000000, 1.000000000000000000 ) ) ;
#136=ORIENTED_EDGE ( 'NONE', *, *, #72395, .F. ) ;
#155=CARTESIAN_POINT ( 'NONE',  ( 47.62500000000000000, 94.53880000000000905, 225.4249999999999829 ) ) ;
#163=AXIS2_PLACEMENT_3D ( 'NONE', #54109, #40507, #5097 ) ;
#182=DIRECTION ( 'NONE',  ( 1.000000000000000000, 0.000000000000000000, 0.000000000000000000 ) ) ;
#188=CARTESIAN_POINT ( 'NONE',  ( -7.661254700127833495, 82.54999999999999716, 275.4630000000000223 ) ) ;
#200=VECTOR ( 'NONE', #2081, 1000.000000000000000 ) ;
#247=SURFACE_STYLE_FILL_AREA ( #77911 ) ;
#278=DIRECTION ( 'NONE',  ( 0.000000000000000000, 0.000000000000000000, -1.000000000000000000 ) ) ;
#293=LINE ( 'NONE', #27992, #72853 ) ;
#295=DIRECTION ( 'NONE',  ( 0.000000000000000000, -1.000000000000000000, 0.000000000000000000 ) ) ;
#301=DIRECTION ( 'NONE',  ( 1.000000000000000000, 0.000000000000000000, -9.299908063537909262E-17 ) ) ;
#364=ORIENTED_EDGE ( 'NONE', *, *, #10443, .F. ) ;
#367=CARTESIAN_POINT ( 'NONE',  ( 8.616376310055921195, 91.75252788878626120, 118.2428346993085313 ) ) ;
#425=DIRECTION ( 'NONE',  ( 0.000000000000000000, 0.000000000000000000, -1.000000000000000000 ) ) ;
#430=VECTOR ( 'NONE', #89507, 1000.000000000000000 ) ;
#445=CARTESIAN_POINT ( 'NONE',  ( 23.75871628398702384, 82.54999999999999716, 298.1325000000000500 ) ) ;
#453=LINE ( 'NONE', #77219, #11024 ) ;
#454=ORIENTED_EDGE ( 'NONE', *, *, #16500, .T. ) ;
#482=FACE_OUTER_BOUND ( 'NONE', #29717, .T. ) ;
#489=CARTESIAN_POINT ( 'NONE',  ( 47.62500000000000000, 111.1250000000000000, 257.1750000000000114 ) ) ;
#490=ORIENTED_EDGE ( 'NONE', *, *, #23966, .T. ) ;
#510=DIRECTION ( 'NONE',  ( 1.000000000000000000, 0.000000000000000000, 0.000000000000000000 ) ) ;
#517=VECTOR ( 'NONE', #25289, 1000.000000000000000 ) ;
#584=CARTESIAN_POINT ( 'NONE',  ( 60.32499999999999574, 82.54999999999999716, 358.0130000000000337 ) ) ;
#605=FACE_OUTER_BOUND ( 'NONE', #87469, .T. ) ;
#647=DIRECTION ( 'NONE',  ( -1.000000000000000000, 0.000000000000000000, 0.000000000000000000 ) ) ;
#703=AXIS2_PLACEMENT_3D ( 'NONE', #37504, #57493, #58381 ) ;
#742=VECTOR ( 'NONE', #7772, 1000.000000000000000 ) ;
#797=ORIENTED_EDGE ( 'NONE', *, *, #47110, .F. ) ;
#799=EDGE_CURVE ( 'NONE', #65439, #55059, #50406, .T. ) ;
#804=EDGE_CURVE ( 'NONE', #2492, #78417, #79484, .T. ) ;
#805=FACE_OUTER_BOUND ( 'NONE', #29803, .T. ) ;
#818=CARTESIAN_POINT ( 'NONE',  ( 0.8322866307615671699, 95.14999999999997726, 118.5559999999999832 ) ) ;
#866=EDGE_CURVE ( 'NONE', #4589, #18695, #41839, .T. ) ;
#874=ORIENTED_EDGE ( 'NONE', *, *, #10631, .F. ) ;
#881=B_SPLINE_CURVE_WITH_KNOTS ( 'NONE', 3,
 ( #17422, #9269, #64236, #16531, #16978, #85591, #23803, #2008, #36967, #71065, #72394, #50588, #2459, #10596, #51039, #38300, #44661, #57403, #43321, #8836, #71948, #85144, #37418, #22911, #51470 ),
 .UNSPECIFIED., .F., .F.,
 ( 4, 2, 2, 2, 2, 2, 2, 2, 2, 1, 2, 2, 4 ),
 ( 0.000000000000000000, 0.002464394434560686874, 0.003696591651841050694, 0.004928788869121414513, 0.007393183303682179450, 0.008625380520962545872, 0.009857577738242914028, 0.01232197217280368330, 0.01355416939008405666, 0.01478636660736442829, 0.01601856382464479991, 0.01725076104192517154, 0.01971515547648590785 ),
 .UNSPECIFIED. ) ;
#949=DIRECTION ( 'NONE',  ( 1.000000000000000000, 0.000000000000000000, 0.000000000000000000 ) ) ;
#950=CARTESIAN_POINT ( 'NONE',  ( 34.92499999999999716, 82.54999999999999716, 290.4490000000000123 ) ) ;
#952=VECTOR ( 'NONE', #55966, 1000.000000000000000 ) ;
#953=FACE_BOUND ( 'NONE', #7835, .T. ) ;
#1035=ORIENTED_EDGE ( 'NONE', *, *, #1775, .F. ) ;
#1091=LINE ( 'NONE', #34257, #64234 ) ;
#1124=APPLICATION_CONTEXT ( 'automotive_design' ) ;
#1129=VERTEX_POINT ( 'NONE', #47992 ) ;
#1160=ORIENTED_EDGE ( 'NONE', *, *, #77085, .F. ) ;
#1171=DIRECTION ( 'NONE',  ( 0.000000000000000000, 0.000000000000000000, -1.000000000000000000 ) ) ;
#1182=PRODUCT_DEFINITION ( 'UNKNOWN', '', #76925, #64183 ) ;
#1197=VERTEX_POINT ( 'NONE', #55253 ) ;
#1210=VECTOR ( 'NONE', #71058, 1000.000000000000000 ) ;
#1257=CYLINDRICAL_SURFACE ( 'NONE', #57135, 3.968749999999992895 ) ;
#1261=DIRECTION ( 'NONE',  ( -0.000000000000000000, -0.000000000000000000, -1.000000000000000000 ) ) ;
#1346=LINE ( 'NONE', #70381, #55192 ) ;
#1350=ORIENTED_EDGE ( 'NONE', *, *, #34749, .F. ) ;
#1395=VERTEX_POINT ( 'NONE', #51577 ) ;
#1426=DIRECTION ( 'NONE',  ( 0.000000000000000000, 0.000000000000000000, 1.000000000000000000 ) ) ;
#1439=DIRECTION ( 'NONE',  ( 0.000000000000000000, 0.000000000000000000, 1.000000000000000000 ) ) ;
#1448=ORIENTED_EDGE ( 'NONE', *, *, #36885, .F. ) ;
#1465=DIRECTION ( 'NONE',  ( 0.000000000000000000, 0.000000000000000000, -1.000000000000000000 ) ) ;
#1589=CARTESIAN_POINT ( 'NONE',  ( 28.57499999999999929, 87.13271776169258942, 310.8325000000000387 ) ) ;
#1612=( NAMED_UNIT ( * ) SI_UNIT ( $, .STERADIAN. ) SOLID_ANGLE_UNIT ( ) );
#1768=VERTEX_POINT ( 'NONE', #64231 ) ;
#1775=EDGE_CURVE ( 'NONE', #14287, #13459, #35615, .T. ) ;
#1814=VERTEX_POINT ( 'NONE', #8372 ) ;
#1893=CARTESIAN_POINT ( 'NONE',  ( 23.08731596616043191, 87.15077889410697765, 301.6545639882101000 ) ) ;
#1904=PRODUCT ( 'Hydraulic Index Locking Pin', 'Hydraulic Index Locking Pin', '', ( #18150 ) ) ;
#1930=EDGE_LOOP ( 'NONE', ( #65051, #37161, #36735, #53971 ) ) ;
#1947=EDGE_LOOP ( 'NONE', ( #11641, #38894 ) ) ;
#2005=DIRECTION ( 'NONE',  ( 0.000000000000000000, 0.000000000000000000, -1.000000000000000000 ) ) ;
#2008=CARTESIAN_POINT ( 'NONE',  ( 11.32175623853374091, 76.95891767344909340, 118.0145928970902816 ) ) ;
#2037=CARTESIAN_POINT ( 'NONE',  ( 88.90000000000000568, 66.67499999999999716, 346.0750000000000455 ) ) ;
#2048=ORIENTED_EDGE ( 'NONE', *, *, #59193, .F. ) ;
#2081=DIRECTION ( 'NONE',  ( -1.092739197465703932E-16, 1.000000000000000000, 0.000000000000000000 ) ) ;
#2108=ORIENTED_EDGE ( 'NONE', *, *, #25100, .T. ) ;
#2109=CIRCLE ( 'NONE', #67309, 8.928100000000000591 ) ;
#2127=ORIENTED_EDGE ( 'NONE', *, *, #59610, .F. ) ;
#2130=CARTESIAN_POINT ( 'NONE',  ( 0.000000000000000000, 65.60000000000000853, 0.000000000000000000 ) ) ;
#2149=ORIENTED_EDGE ( 'NONE', *, *, #11022, .T. ) ;
#2176=FACE_OUTER_BOUND ( 'NONE', #18334, .T. ) ;
#2207=FACE_OUTER_BOUND ( 'NONE', #61381, .T. ) ;
#2216=ORIENTED_EDGE ( 'NONE', *, *, #77802, .T. ) ;
#2285=CARTESIAN_POINT ( 'NONE',  ( 47.62500000000000000, 66.67499999999999716, 292.1000000000000227 ) ) ;
#2319=DIRECTION ( 'NONE',  ( 0.000000000000000000, -1.000000000000000000, 0.000000000000000000 ) ) ;
#2327=CARTESIAN_POINT ( 'NONE',  ( 47.62500000000000000, 69.84999999999999432, 288.9250000000000114 ) ) ;
#2345=CARTESIAN_POINT ( 'NONE',  ( 23.18046939137932583, 86.82760181162625202, 305.0120167406822702 ) ) ;
#2347=EDGE_CURVE ( 'NONE', #70579, #56973, #88091, .T. ) ;
#2459=CARTESIAN_POINT ( 'NONE',  ( 9.196777273860476498, 73.92746944614621896, 118.1991088758754813 ) ) ;
#2492=VERTEX_POINT ( 'NONE', #35841 ) ;
#2567=CARTESIAN_POINT ( 'NONE',  ( 57.14999999999999858, 60.86974387893089755, 323.0879999999999654 ) ) ;
#2582=LINE ( 'NONE', #30278, #40896 ) ;
#2660=CARTESIAN_POINT ( 'NONE',  ( 7.661254700127822836, 98.64746158385918307, 275.4630000000000223 ) ) ;
#2680=DIRECTION ( 'NONE',  ( 0.000000000000000000, 0.000000000000000000, -1.000000000000000000 ) ) ;
#2689=VECTOR ( 'NONE', #77875, 1000.000000000000000 ) ;
#2690=FACE_OUTER_BOUND ( 'NONE', #33003, .T. ) ;
#2729=LINE ( 'NONE', #78601, #83208 ) ;
#2732=EDGE_CURVE ( 'NONE', #70235, #30868, #67125, .T. ) ;
#2744=EDGE_CURVE ( 'NONE', #18726, #80899, #47888, .T. ) ;
#2761=CARTESIAN_POINT ( 'NONE',  ( 38.10000000000000142, 95.25000000000000000, 283.4005000000000223 ) ) ;
#2763=ORIENTED_EDGE ( 'NONE', *, *, #21714, .T. ) ;
#2767=CARTESIAN_POINT ( 'NONE',  ( 47.62500000000000000, 73.02500000000000568, 219.0749999999999886 ) ) ;
#2783=PLANE ( 'NONE',  #22479 ) ;
#2807=CARTESIAN_POINT ( 'NONE',  ( 6.938893903907229955E-15, 50.79999999999999716, 216.0269999999999868 ) ) ;
#2821=DIRECTION ( 'NONE',  ( 0.000000000000000000, -1.000000000000000000, 0.000000000000000000 ) ) ;
#2884=LINE ( 'NONE', #51017, #12434 ) ;
#2897=CARTESIAN_POINT ( 'NONE',  ( 52.38749999999999574, 94.53880000000000905, 250.8250000000000171 ) ) ;
#2915=EDGE_CURVE ( 'NONE', #28761, #77463, #23377, .T. ) ;
#2923=CARTESIAN_POINT ( 'NONE',  ( 0.000000000000000000, 67.86880000000000734, 259.9944000000000415 ) ) ;
#2937=ORIENTED_EDGE ( 'NONE', *, *, #22747, .T. ) ;
#2994=DIRECTION ( 'NONE',  ( 1.000000000000000000, 0.000000000000000000, 0.000000000000000000 ) ) ;
#3079=ADVANCED_FACE ( 'NONE', ( #55042, #19655 ), #26033, .F. ) ;
#3099=CARTESIAN_POINT ( 'NONE',  ( 47.62500000000000000, 69.84999999999999432, 292.1000000000000227 ) ) ;
#3123=EDGE_CURVE ( 'NONE', #59883, #27284, #6049, .T. ) ;
#3152=ORIENTED_EDGE ( 'NONE', *, *, #799, .T. ) ;
#3163=EDGE_CURVE ( 'NONE', #17742, #41217, #13740, .T. ) ;
#3186=CARTESIAN_POINT ( 'NONE',  ( 82.54999999999999716, 95.25000000000000000, 280.2255000000000109 ) ) ;
#3348=FACE_OUTER_BOUND ( 'NONE', #21113, .T. ) ;
#3354=ORIENTED_EDGE ( 'NONE', *, *, #70618, .F. ) ;
#3376=ORIENTED_EDGE ( 'NONE', *, *, #64892, .F. ) ;
#3437=CARTESIAN_POINT ( 'NONE',  ( -44.45000000000000284, 50.79999999999999716, 206.3750000000000000 ) ) ;
#3472=CARTESIAN_POINT ( 'NONE',  ( 57.14999999999999858, 69.84999999999999432, 323.0879999999999654 ) ) ;
#3489=ORIENTED_EDGE ( 'NONE', *, *, #1775, .T. ) ;
#3505=DIRECTION ( 'NONE',  ( 0.000000000000000000, -1.000000000000000000, 0.000000000000000000 ) ) ;
#3507=ORIENTED_EDGE ( 'NONE', *, *, #4307, .T. ) ;
#3531=ORIENTED_EDGE ( 'NONE', *, *, #47110, .T. ) ;
#3560=AXIS2_PLACEMENT_3D ( 'NONE', #18472, #58464, #67077 ) ;
#3566=DIRECTION ( 'NONE',  ( 1.000000000000000000, 0.000000000000000000, 0.000000000000000000 ) ) ;
#3575=LINE ( 'NONE', #17660, #7097 ) ;
#3577=EDGE_CURVE ( 'NONE', #66754, #16125, #18204, .T. ) ;
#3589=EDGE_LOOP ( 'NONE', ( #36625, #20781, #42240, #17760 ) ) ;
#3607=AXIS2_PLACEMENT_3D ( 'NONE', #78386, #70661, #1171 ) ;
#3646=FACE_OUTER_BOUND ( 'NONE', #46762, .T. ) ;
#3739=CARTESIAN_POINT ( 'NONE',  ( 47.62500000000000000, 111.1250000000000000, 257.1750000000000114 ) ) ;
#3773=DIRECTION ( 'NONE',  ( 0.000000000000000000, -0.5000000000000007772, 0.8660254037844381525 ) ) ;
#3784=VECTOR ( 'NONE', #77088, 1000.000000000000000 ) ;
#3790=DIRECTION ( 'NONE',  ( 0.000000000000000000, 1.000000000000000000, 0.000000000000000000 ) ) ;
#3886=DIRECTION ( 'NONE',  ( 0.000000000000000000, -1.000000000000000000, 0.000000000000000000 ) ) ;
#3897=VERTEX_POINT ( 'NONE', #78572 ) ;
#3948=LINE ( 'NONE', #31649, #78956 ) ;
#3978=ORIENTED_EDGE ( 'NONE', *, *, #866, .F. ) ;
#3987=DIRECTION ( 'NONE',  ( 0.000000000000000000, 0.000000000000000000, -1.000000000000000000 ) ) ;
#4033=ORIENTED_EDGE ( 'NONE', *, *, #33159, .T. ) ;
#4063=FACE_OUTER_BOUND ( 'NONE', #32493, .T. ) ;
#4072=EDGE_LOOP ( 'NONE', ( #12695, #78909 ) ) ;
#4116=ADVANCED_FACE ( 'NONE', ( #87154 ), #18998, .F. ) ;
#4174=ORIENTED_EDGE ( 'NONE', *, *, #74964, .F. ) ;
#4268=LINE ( 'NONE', #59656, #67666 ) ;
#4307=EDGE_CURVE ( 'NONE', #70385, #9455, #35083, .T. ) ;
#4355=CARTESIAN_POINT ( 'NONE',  ( -7.661254700127829942, 66.45253841614081125, 275.4630000000000223 ) ) ;
#4375=LINE ( 'NONE', #19787, #8114 ) ;
#4377=ORIENTED_EDGE ( 'NONE', *, *, #50333, .T. ) ;
#4379=EDGE_CURVE ( 'NONE', #13459, #54369, #44796, .T. ) ;
#4428=CARTESIAN_POINT ( 'NONE',  ( 57.14999999999999858, 95.25000000000000000, 304.0379999999999541 ) ) ;
#4430=AXIS2_PLACEMENT_3D ( 'NONE', #64080, #9119, #949 ) ;
#4477=EDGE_CURVE ( 'NONE', #29470, #28274, #76239, .T. ) ;
#4497=AXIS2_PLACEMENT_3D ( 'NONE', #52951, #65293, #23965 ) ;
#4499=VERTEX_POINT ( 'NONE', #17553 ) ;
#4583=CARTESIAN_POINT ( 'NONE',  ( 23.22033092422023159, 78.41772510193747792, 300.5067426286719297 ) ) ;
#4589=VERTEX_POINT ( 'NONE', #36947 ) ;
#4619=DIRECTION ( 'NONE',  ( 0.000000000000000000, 0.000000000000000000, -1.000000000000000000 ) ) ;
#4625=ORIENTED_EDGE ( 'NONE', *, *, #59195, .F. ) ;
#4629=DIRECTION ( 'NONE',  ( -0.000000000000000000, -0.000000000000000000, -1.000000000000000000 ) ) ;
#4641=ORIENTED_EDGE ( 'NONE', *, *, #33159, .F. ) ;
#4672=EDGE_CURVE ( 'NONE', #85158, #68630, #2884, .T. ) ;
#4859=ORIENTED_EDGE ( 'NONE', *, *, #12120, .T. ) ;
#4902=ORIENTED_EDGE ( 'NONE', *, *, #60403, .F. ) ;
#4959=CARTESIAN_POINT ( 'NONE',  ( 57.14999999999999858, 60.86974387893089755, 326.2630000000000337 ) ) ;
#4977=DIRECTION ( 'NONE',  ( 0.000000000000000000, -1.000000000000000000, 0.000000000000000000 ) ) ;
#5079=VECTOR ( 'NONE', #48586, 1000.000000000000000 ) ;
#5097=DIRECTION ( 'NONE',  ( 0.000000000000000000, 0.000000000000000000, -1.000000000000000000 ) ) ;
#5147=CARTESIAN_POINT ( 'NONE',  ( 50.79999999999999716, 69.84999999999999432, 257.1750000000000114 ) ) ;
#5239=DIRECTION ( 'NONE',  ( 0.000000000000000000, -1.000000000000000000, 0.000000000000000000 ) ) ;
#5250=EDGE_CURVE ( 'NONE', #52977, #6408, #68975, .T. ) ;
#5310=EDGE_CURVE ( 'NONE', #27284, #47135, #33535, .T. ) ;
#5325=EDGE_LOOP ( 'NONE', ( #77996, #11515, #17710, #80426, #77333 ) ) ;
#5392=EDGE_CURVE ( 'NONE', #68630, #79853, #74132, .T. ) ;
#5496=ADVANCED_FACE ( 'NONE', ( #72111 ), #37592, .T. ) ;
#5521=DIRECTION ( 'NONE',  ( 0.000000000000000000, 0.000000000000000000, -1.000000000000000000 ) ) ;
#5554=VECTOR ( 'NONE', #88031, 1000.000000000000000 ) ;
#5642=DIRECTION ( 'NONE',  ( 1.000000000000000000, 0.000000000000000000, 0.000000000000000000 ) ) ;
#5650=CARTESIAN_POINT ( 'NONE',  ( -12.59999999999999964, 82.54999999999999716, -190.5010000000000048 ) ) ;
#5662=LINE ( 'NONE', #74689, #18801 ) ;
#5753=DIRECTION ( 'NONE',  ( 1.000000000000000000, 0.000000000000000000, 0.000000000000000000 ) ) ;
#5760=CARTESIAN_POINT ( 'NONE',  ( 0.000000000000000000, 50.79999999999999716, 265.5569999999999595 ) ) ;
#5772=DIRECTION ( 'NONE',  ( 1.000000000000000000, 0.000000000000000000, 0.000000000000000000 ) ) ;
#5815=DIRECTION ( 'NONE',  ( 0.000000000000000000, 1.000000000000000000, 0.000000000000000000 ) ) ;
#5820=CARTESIAN_POINT ( 'NONE',  ( 57.14999999999999858, 69.84999999999999432, 280.2255000000000109 ) ) ;
#5861=DIRECTION ( 'NONE',  ( 0.000000000000000000, 0.000000000000000000, -1.000000000000000000 ) ) ;
#5871=DIRECTION ( 'NONE',  ( -1.000000000000000000, 0.000000000000000000, -9.713237310806269221E-16 ) ) ;
#5933=ADVANCED_FACE ( 'NONE', ( #31543 ), #33601, .F. ) ;
#5934=CARTESIAN_POINT ( 'NONE',  ( 47.62500000000000000, 111.1250000000000000, 257.1750000000000114 ) ) ;
#5943=ORIENTED_EDGE ( 'NONE', *, *, #9393, .T. ) ;
#5971=DIRECTION ( 'NONE',  ( -1.000000000000000000, 0.000000000000000000, 0.000000000000000000 ) ) ;
#5992=PRESENTATION_STYLE_ASSIGNMENT (( #68209 ) ) ;
#5993=DIRECTION ( 'NONE',  ( 0.000000000000000000, 1.000000000000000000, 0.000000000000000000 ) ) ;
#6016=VECTOR ( 'NONE', #12823, 1000.000000000000000 ) ;
#6049=LINE ( 'NONE', #12398, #89676 ) ;
#6058=CARTESIAN_POINT ( 'NONE',  ( -7.674860457568732031, 92.55144245102577827, 118.3077557055132161 ) ) ;
#6108=CARTESIAN_POINT ( 'NONE',  ( 88.90000000000000568, 66.67499999999999716, 244.4749999999999943 ) ) ;
#6174=ORIENTED_EDGE ( 'NONE', *, *, #42937, .F. ) ;
#6190=DIRECTION ( 'NONE',  ( 0.000000000000000000, 0.000000000000000000, 1.000000000000000000 ) ) ;
#6237=VECTOR ( 'NONE', #52625, 999.9999999999998863 ) ;
#6258=ORIENTED_EDGE ( 'NONE', *, *, #53593, .T. ) ;
#6283=DIRECTION ( 'NONE',  ( 0.000000000000000000, 0.000000000000000000, 1.000000000000000000 ) ) ;
#6337=EDGE_CURVE ( 'NONE', #70385, #70167, #10112, .T. ) ;
#6364=CARTESIAN_POINT ( 'NONE',  ( 23.11218988842089672, 78.03196636687118826, 304.4337129636800796 ) ) ;
#6382=DIRECTION ( 'NONE',  ( -1.000000000000000000, 0.000000000000000000, 0.000000000000000000 ) ) ;
#6408=VERTEX_POINT ( 'NONE', #36923 ) ;
#6453=LINE ( 'NONE', #61843, #54934 ) ;
#6483=CARTESIAN_POINT ( 'NONE',  ( -1.652225533659690049, 95.06819236710590815, 118.5472263177064889 ) ) ;
#6571=CARTESIAN_POINT ( 'NONE',  ( 28.57499999999999929, 77.96728223830730542, 294.9574999999999818 ) ) ;
#6581=EDGE_LOOP ( 'NONE', ( #41739, #16307, #89460, #44337 ) ) ;
#6664=ORIENTED_EDGE ( 'NONE', *, *, #58592, .F. ) ;
#6689=CYLINDRICAL_SURFACE ( 'NONE', #20563, 3.174999999999983391 ) ;
#6698=EDGE_LOOP ( 'NONE', ( #20480, #67587, #30407, #21376, #27468 ) ) ;
#6702=ORIENTED_EDGE ( 'NONE', *, *, #27816, .T. ) ;
#6742=CARTESIAN_POINT ( 'NONE',  ( -44.45000000000000284, 114.2999999999999972, 275.4630000000000223 ) ) ;
#6785=DIRECTION ( 'NONE',  ( 0.000000000000000000, 1.000000000000000000, 0.000000000000000000 ) ) ;
#6800=DIRECTION ( 'NONE',  ( 0.000000000000000000, 0.000000000000000000, -1.000000000000000000 ) ) ;
#6822=LINE ( 'NONE', #61768, #430 ) ;
#6840=CARTESIAN_POINT ( 'NONE',  ( 7.661254700127833495, 82.54999999999999716, 317.6630000000000109 ) ) ;
#6853=ADVANCED_FACE ( 'NONE', ( #65849 ), #58583, .F. ) ;
#6861=DIRECTION ( 'NONE',  ( 0.000000000000000000, 0.000000000000000000, 1.000000000000000000 ) ) ;
#6898=VECTOR ( 'NONE', #7808, 1000.000000000000000 ) ;
#6912=CARTESIAN_POINT ( 'NONE',  ( 60.32499999999999574, 82.54999999999999716, 335.3740053999999304 ) ) ;
#6934=CARTESIAN_POINT ( 'NONE',  ( -11.93654268304338650, 86.60576128432494158, 117.9536290563174674 ) ) ;
#7097=VECTOR ( 'NONE', #45335, 1000.000000000000000 ) ;
#7098=DIRECTION ( 'NONE',  ( 0.000000000000000000, -1.000000000000000000, 0.000000000000000000 ) ) ;
#7113=DIRECTION ( 'NONE',  ( 0.000000000000000000, 0.000000000000000000, 1.000000000000000000 ) ) ;
#7177=DIRECTION ( 'NONE',  ( -1.000000000000000000, 0.000000000000000000, 0.000000000000000000 ) ) ;
#7178=ORIENTED_EDGE ( 'NONE', *, *, #49138, .T. ) ;
#7191=CARTESIAN_POINT ( 'NONE',  ( 0.000000000000000000, 50.79999999999999716, 265.5569999999999595 ) ) ;
#7212=EDGE_LOOP ( 'NONE', ( #25505, #37112, #454, #32977 ) ) ;
#7222=ORIENTED_EDGE ( 'NONE', *, *, #56888, .T. ) ;
#7292=DIRECTION ( 'NONE',  ( 0.000000000000000000, 1.000000000000000000, 0.000000000000000000 ) ) ;
#7301=EDGE_CURVE ( 'NONE', #6408, #46574, #73798, .T. ) ;
#7372=ORIENTED_EDGE ( 'NONE', *, *, #4672, .F. ) ;
#7395=AXIS2_PLACEMENT_3D ( 'NONE', #64411, #42155, #77151 ) ;
#7416=ORIENTED_EDGE ( 'NONE', *, *, #44096, .F. ) ;
#7425=CARTESIAN_POINT ( 'NONE',  ( 20.75871628398702384, 82.54999999999999716, 320.6630000000000109 ) ) ;
#7474=AXIS2_PLACEMENT_3D ( 'NONE', #77017, #14797, #62475 ) ;
#7537=DIRECTION ( 'NONE',  ( 0.000000000000000000, 0.000000000000000000, -1.000000000000000000 ) ) ;
#7573=EDGE_CURVE ( 'NONE', #12738, #4589, #76938, .T. ) ;
#7588=DIRECTION ( 'NONE',  ( 0.000000000000000000, 0.000000000000000000, -1.000000000000000000 ) ) ;
#7634=CARTESIAN_POINT ( 'NONE',  ( 4.049525628232704122, 94.48868704156625142, 118.4874810299777437 ) ) ;
#7668=VERTEX_POINT ( 'NONE', #59586 ) ;
#7739=DIRECTION ( 'NONE',  ( 1.000000000000000000, 0.000000000000000000, 0.000000000000000000 ) ) ;
#7761=EDGE_CURVE ( 'NONE', #1197, #4589, #89117, .T. ) ;
#7772=DIRECTION ( 'NONE',  ( 1.986798540846734824E-16, 0.000000000000000000, -1.000000000000000000 ) ) ;
#7807=ADVANCED_FACE ( 'NONE', ( #20079 ), #47753, .F. ) ;
#7808=DIRECTION ( 'NONE',  ( 0.000000000000000000, -1.000000000000000000, 0.000000000000000000 ) ) ;
#7817=LINE ( 'NONE', #14646, #41625 ) ;
#7823=VERTEX_POINT ( 'NONE', #46848 ) ;
#7835=EDGE_LOOP ( 'NONE', ( #49339, #29904 ) ) ;
#7871=DIRECTION ( 'NONE',  ( 1.000000000000000000, 0.000000000000000000, 0.000000000000000000 ) ) ;
#7875=ADVANCED_FACE ( 'NONE', ( #67308 ), #18269, .F. ) ;
#7876=VECTOR ( 'NONE', #21171, 1000.000000000000000 ) ;
#7890=DIRECTION ( 'NONE',  ( 0.000000000000000000, 0.4999999999999995004, -0.8660254037844390407 ) ) ;
#7904=AXIS2_PLACEMENT_3D ( 'NONE', #83592, #10723, #65256 ) ;
#7913=CARTESIAN_POINT ( 'NONE',  ( -44.45000000000000284, 50.79999999999999716, 206.3750000000000000 ) ) ;
#7917=EDGE_CURVE ( 'NONE', #3897, #50079, #75033, .T. ) ;
#7940=CIRCLE ( 'NONE', #61613, 5.562600000000000655 ) ;
#7953=CARTESIAN_POINT ( 'NONE',  ( 45.66030316258350297, 82.54999999999999716, 346.9005000000000223 ) ) ;
#7980=CYLINDRICAL_SURFACE ( 'NONE', #47642, 3.000000000000002665 ) ;
#8005=ORIENTED_EDGE ( 'NONE', *, *, #2744, .T. ) ;
#8018=DIRECTION ( 'NONE',  ( 1.000000000000000000, 0.000000000000000000, -1.821231995776179916E-16 ) ) ;
#8031=DIRECTION ( 'NONE',  ( 0.000000000000000000, -1.000000000000000000, 0.000000000000000000 ) ) ;
#8057=EDGE_CURVE ( 'NONE', #66754, #75737, #56363, .T. ) ;
#8078=LINE ( 'NONE', #27617, #67041 ) ;
#8086=DIRECTION ( 'NONE',  ( 0.000000000000000000, 0.000000000000000000, -1.000000000000000000 ) ) ;
#8089=DIRECTION ( 'NONE',  ( 0.000000000000000000, 0.000000000000000000, -1.000000000000000000 ) ) ;
#8099=CARTESIAN_POINT ( 'NONE',  ( 0.000000000000000000, 82.54999999999999716, 206.3750000000000000 ) ) ;
#8114=VECTOR ( 'NONE', #47016, 1000.000000000000000 ) ;
#8138=DIRECTION ( 'NONE',  ( -1.000000000000000000, 0.000000000000000000, 9.299908063537909262E-17 ) ) ;
#8155=DIRECTION ( 'NONE',  ( 0.000000000000000000, -0.5150380749100549327, -0.8571673007021118895 ) ) ;
#8277=AXIS2_PLACEMENT_3D ( 'NONE', #9537, #35892, #76786 ) ;
#8284=CARTESIAN_POINT ( 'NONE',  ( 82.54999999999999716, 95.25000000000000000, 280.2255000000000109 ) ) ;
#8352=ORIENTED_EDGE ( 'NONE', *, *, #44355, .F. ) ;
#8366=VECTOR ( 'NONE', #75704, 1000.000000000000000 ) ;
#8367=ORIENTED_EDGE ( 'NONE', *, *, #34749, .T. ) ;
#8372=CARTESIAN_POINT ( 'NONE',  ( 60.32499999999999574, 82.54999999999999716, 330.0094617072599590 ) ) ;
#8383=ORIENTED_EDGE ( 'NONE', *, *, #4307, .F. ) ;
#8422=SURFACE_STYLE_USAGE ( .BOTH. , #49732 ) ;
#8489=CARTESIAN_POINT ( 'NONE',  ( 34.92499999999999716, 82.54999999999999716, 302.8950000000000387 ) ) ;
#8511=VECTOR ( 'NONE', #47048, 1000.000000000000000 ) ;
#8584=ORIENTED_EDGE ( 'NONE', *, *, #84149, .F. ) ;
#8602=ORIENTED_EDGE ( 'NONE', *, *, #69802, .F. ) ;
#8603=ORIENTED_EDGE ( 'NONE', *, *, #40169, .F. ) ;
#8687=DIRECTION ( 'NONE',  ( 0.000000000000000000, 1.000000000000000000, 0.000000000000000000 ) ) ;
#8702=FACE_OUTER_BOUND ( 'NONE', #44461, .T. ) ;
#8721=CARTESIAN_POINT ( 'NONE',  ( 23.22106422052441133, 86.67941937331816860, 305.2876845235662699 ) ) ;
#8739=DIRECTION ( 'NONE',  ( 0.000000000000000000, 0.000000000000000000, 1.000000000000000000 ) ) ;
#8765=AXIS2_PLACEMENT_3D ( 'NONE', #53918, #5815, #11725 ) ;
#8836=CARTESIAN_POINT ( 'NONE',  ( 4.055565339044333584, 70.61339494146574225, 118.4872713058879441 ) ) ;
#8926=VERTEX_POINT ( 'NONE', #57898 ) ;
#8934=CARTESIAN_POINT ( 'NONE',  ( 52.38749999999999574, 94.53880000000000905, 225.4249999999999829 ) ) ;
#8996=DIRECTION ( 'NONE',  ( 0.000000000000000000, -1.000000000000000000, 0.000000000000000000 ) ) ;
#9119=DIRECTION ( 'NONE',  ( 0.000000000000000000, 0.000000000000000000, 1.000000000000000000 ) ) ;
#9147=DIRECTION ( 'NONE',  ( 0.000000000000000000, -1.000000000000000000, 0.000000000000000000 ) ) ;
#9168=ORIENTED_EDGE ( 'NONE', *, *, #31013, .F. ) ;
#9192=LINE ( 'NONE', #76884, #76923 ) ;
#9241=AXIS2_PLACEMENT_3D ( 'NONE', #70346, #57144, #83531 ) ;
#9269=CARTESIAN_POINT ( 'NONE',  ( 12.60000000000000497, 81.71666160541465729, 117.8845415480757879 ) ) ;
#9308=CONICAL_SURFACE ( 'NONE', #16567, 8.928100000000000591, 1.029744258676653645 ) ;
#9332=CARTESIAN_POINT ( 'NONE',  ( 52.99265158129170317, 95.25000000000000000, 346.9005000000000223 ) ) ;
#9360=DIRECTION ( 'NONE',  ( -1.821231995776179916E-16, 0.000000000000000000, -1.000000000000000000 ) ) ;
#9393=EDGE_CURVE ( 'NONE', #86161, #37287, #73703, .T. ) ;
#9455=VERTEX_POINT ( 'NONE', #80989 ) ;
#9457=ORIENTED_EDGE ( 'NONE', *, *, #30218, .T. ) ;
#9482=DIRECTION ( 'NONE',  ( 0.000000000000000000, -1.000000000000000000, 0.000000000000000000 ) ) ;
#9537=CARTESIAN_POINT ( 'NONE',  ( 7.661254700127822836, 95.64746158385918307, 317.6630000000000109 ) ) ;
#9538=CARTESIAN_POINT ( 'NONE',  ( 88.90000000000000568, 69.84999999999999432, 346.0750000000000455 ) ) ;
#9568=CARTESIAN_POINT ( 'NONE',  ( 28.57499999999999929, 82.54999999999999716, 307.6574999999999704 ) ) ;
#9579=ORIENTED_EDGE ( 'NONE', *, *, #52583, .F. ) ;
#9581=DIRECTION ( 'NONE',  ( 0.000000000000000000, 0.000000000000000000, 1.000000000000000000 ) ) ;
#9612=VECTOR ( 'NONE', #76064, 1000.000000000000000 ) ;
#9676=AXIS2_PLACEMENT_3D ( 'NONE', #28248, #22808, #1465 ) ;
#9697=VECTOR ( 'NONE', #73084, 1000.000000000000000 ) ;
#9742=EDGE_CURVE ( 'NONE', #52329, #85158, #7940, .T. ) ;
#9743=AXIS2_PLACEMENT_3D ( 'NONE', #36746, #65337, #38076 ) ;
#9799=ADVANCED_FACE ( 'NONE', ( #78205 ), #2783, .T. ) ;
#9802=EDGE_CURVE ( 'NONE', #52977, #50184, #65443, .T. ) ;
#9834=DIRECTION ( 'NONE',  ( 0.000000000000000000, 0.000000000000000000, -1.000000000000000000 ) ) ;
#9908=ADVANCED_FACE ( 'NONE', ( #74039 ), #46758, .F. ) ;
#9915=DIRECTION ( 'NONE',  ( -1.000000000000000000, 0.000000000000000000, 0.000000000000000000 ) ) ;
#9947=VECTOR ( 'NONE', #15211, 1000.000000000000000 ) ;
#9969=ORIENTED_EDGE ( 'NONE', *, *, #48563, .T. ) ;
#10006=LINE ( 'NONE', #24526, #24400 ) ;
#10021=LINE ( 'NONE', #23229, #70117 ) ;
#10033=ADVANCED_FACE ( 'NONE', ( #35726 ), #28281, .F. ) ;
#10040=DIRECTION ( 'NONE',  ( 0.000000000000000000, -1.000000000000000000, 0.000000000000000000 ) ) ;
#10049=CARTESIAN_POINT ( 'NONE',  ( 23.71360729876448303, 83.79303145207032344, 307.5031054200276799 ) ) ;
#10112=LINE ( 'NONE', #59131, #62647 ) ;
#10129=VERTEX_POINT ( 'NONE', #63903 ) ;
#10146=VECTOR ( 'NONE', #86718, 1000.000000000000000 ) ;
#10153=CYLINDRICAL_SURFACE ( 'NONE', #12875, 3.968750000000020872 ) ;
#10223=LINE ( 'NONE', #39262, #35801 ) ;
#10249=EDGE_CURVE ( 'NONE', #59883, #72947, #19877, .T. ) ;
#10259=LINE ( 'NONE', #32027, #31192 ) ;
#10299=EDGE_LOOP ( 'NONE', ( #70905, #1160, #4174, #80190 ) ) ;
#10305=LINE ( 'NONE', #66598, #78501 ) ;
#10308=EDGE_CURVE ( 'NONE', #56609, #53213, #65232, .T. ) ;
#10313=CYLINDRICAL_SURFACE ( 'NONE', #14047, 3.174999999999983391 ) ;
#10322=DIRECTION ( 'NONE',  ( 0.000000000000000000, -1.000000000000000000, 0.000000000000000000 ) ) ;
#10351=CARTESIAN_POINT ( 'NONE',  ( 47.62500000000000000, 94.53880000000000905, 250.8250000000000171 ) ) ;
#10443=EDGE_CURVE ( 'NONE', #62569, #85065, #88103, .T. ) ;
#10506=VECTOR ( 'NONE', #81501, 1000.000000000000000 ) ;
#10508=CARTESIAN_POINT ( 'NONE',  ( 52.38749999999999574, 94.53880000000000905, 221.4562499999999829 ) ) ;
#10524=ORIENTED_EDGE ( 'NONE', *, *, #68571, .T. ) ;
#10540=ORIENTED_EDGE ( 'NONE', *, *, #84842, .F. ) ;
#10596=CARTESIAN_POINT ( 'NONE',  ( 8.325040720630020985, 73.05638748903209034, 118.2647812922514987 ) ) ;
#10609=ORIENTED_EDGE ( 'NONE', *, *, #66890, .T. ) ;
#10621=FACE_OUTER_BOUND ( 'NONE', #75644, .T. ) ;
#10631=EDGE_CURVE ( 'NONE', #17742, #10129, #17029, .T. ) ;
#10706=DIRECTION ( 'NONE',  ( 0.000000000000000000, -1.000000000000000000, 0.000000000000000000 ) ) ;
#10723=DIRECTION ( 'NONE',  ( 0.000000000000000000, -1.000000000000000000, 0.000000000000000000 ) ) ;
#10771=CARTESIAN_POINT ( 'NONE',  ( 44.45000000000000284, 50.79999999999999716, 206.3750000000000000 ) ) ;
#10777=CONICAL_SURFACE ( 'NONE', #86210, 6.858000000000003205, 0.02993239667170383839 ) ;
#10779=ORIENTED_EDGE ( 'NONE', *, *, #42102, .T. ) ;
#10806=ORIENTED_EDGE ( 'NONE', *, *, #9802, .T. ) ;
#10846=VECTOR ( 'NONE', #84197, 1000.000000000000000 ) ;
#10854=CYLINDRICAL_SURFACE ( 'NONE', #70881, 4.762500000000002842 ) ;
#10908=ADVANCED_FACE ( 'NONE', ( #27352 ), #32822, .F. ) ;
#10916=DIRECTION ( 'NONE',  ( 0.000000000000000000, 0.000000000000000000, -1.000000000000000000 ) ) ;
#10936=EDGE_LOOP ( 'NONE', ( #6174, #2108, #10609, #33361 ) ) ;
#11022=EDGE_CURVE ( 'NONE', #52329, #79853, #56836, .T. ) ;
#11024=VECTOR ( 'NONE', #55391, 1000.000000000000000 ) ;
#11058=ORIENTED_EDGE ( 'NONE', *, *, #12443, .F. ) ;
#11133=CARTESIAN_POINT ( 'NONE',  ( 44.45000000000000284, 69.84999999999999432, 219.0749999999999886 ) ) ;
#11136=ORIENTED_EDGE ( 'NONE', *, *, #13699, .T. ) ;
#11147=CARTESIAN_POINT ( 'NONE',  ( 7.760385678595139561E-15, 60.82030000000000314, 222.5849787991094786 ) ) ;
#11185=LINE ( 'NONE', #17566, #47519 ) ;
#11194=AXIS2_PLACEMENT_3D ( 'NONE', #75307, #59860, #61218 ) ;
#11215=EDGE_CURVE ( 'NONE', #76329, #50184, #45870, .T. ) ;
#11267=LINE ( 'NONE', #26683, #5554 ) ;
#11281=CARTESIAN_POINT ( 'NONE',  ( 57.14999999999999858, 69.84999999999999432, 280.2255000000000109 ) ) ;
#11283=CARTESIAN_POINT ( 'NONE',  ( 52.38749999999999574, 94.53880000000000905, 221.4562499999999829 ) ) ;
#11328=EDGE_CURVE ( 'NONE', #24990, #69696, #66784, .T. ) ;
#11379=PLANE ( 'NONE',  #38591 ) ;
#11393=CARTESIAN_POINT ( 'NONE',  ( 23.04768281101732796, 77.81817409959050735, 302.2712646479865271 ) ) ;
#11394=CARTESIAN_POINT ( 'NONE',  ( 53.97500000000000142, 95.25000000000000000, 283.4005000000000223 ) ) ;
#11424=FACE_OUTER_BOUND ( 'NONE', #41978, .T. ) ;
#11515=ORIENTED_EDGE ( 'NONE', *, *, #24549, .T. ) ;
#11532=ORIENTED_EDGE ( 'NONE', *, *, #25998, .T. ) ;
#11545=CARTESIAN_POINT ( 'NONE',  ( 31.75000000000000000, 66.67499999999999716, 295.2750000000000341 ) ) ;
#11546=ORIENTED_EDGE ( 'NONE', *, *, #67266, .F. ) ;
#11560=CARTESIAN_POINT ( 'NONE',  ( 28.57499999999999929, 77.96728223830740490, 310.8325000000000387 ) ) ;
#11575=VERTEX_POINT ( 'NONE', #38520 ) ;
#11617=ORIENTED_EDGE ( 'NONE', *, *, #59812, .T. ) ;
#11634=CARTESIAN_POINT ( 'NONE',  ( 85.72499999999999432, 69.84999999999999432, 342.8999999999999773 ) ) ;
#11641=ORIENTED_EDGE ( 'NONE', *, *, #2347, .F. ) ;
#11716=FACE_OUTER_BOUND ( 'NONE', #33770, .T. ) ;
#11718=DIRECTION ( 'NONE',  ( 0.000000000000000000, 1.000000000000000000, 6.056575390184510167E-15 ) ) ;
#11725=DIRECTION ( 'NONE',  ( 0.000000000000000000, 0.000000000000000000, 1.000000000000000000 ) ) ;
#11735=CIRCLE ( 'NONE', #62502, 3.968750000000020872 ) ;
#11762=EDGE_CURVE ( 'NONE', #31158, #15433, #11267, .T. ) ;
#11769=CARTESIAN_POINT ( 'NONE',  ( -7.661254700127833495, 69.45253841614081125, 317.6630000000000109 ) ) ;
#11791=AXIS2_PLACEMENT_3D ( 'NONE', #56899, #84637, #21962 ) ;
#11846=CARTESIAN_POINT ( 'NONE',  ( 23.08473575203844064, 77.94038194589714408, 301.6578082054804213 ) ) ;
#11868=DIRECTION ( 'NONE',  ( 0.000000000000000000, 1.000000000000000000, 0.000000000000000000 ) ) ;
#11873=VECTOR ( 'NONE', #21298, 999.9999999999998863 ) ;
#11902=DIRECTION ( 'NONE',  ( 0.000000000000000000, 0.000000000000000000, 1.000000000000000000 ) ) ;
#11906=CARTESIAN_POINT ( 'NONE',  ( 88.90000000000000568, 69.84999999999999432, 346.0750000000000455 ) ) ;
#11913=CIRCLE ( 'NONE', #17682, 3.968749999999992895 ) ;
#11919=ADVANCED_FACE ( 'NONE', ( #42541 ), #77097, .F. ) ;
#11971=CARTESIAN_POINT ( 'NONE',  ( -12.27785138262897924, 85.41117304334655103, 117.9185570544176898 ) ) ;
#11994=CARTESIAN_POINT ( 'NONE',  ( 34.92499999999999716, 66.67499999999999716, 292.1000000000000227 ) ) ;
#12008=CARTESIAN_POINT ( 'NONE',  ( 82.54999999999999716, 69.84999999999999432, 346.9005000000000223 ) ) ;
#12024=CARTESIAN_POINT ( 'NONE',  ( 44.45000000000000284, 111.1250000000000000, 219.0749999999999886 ) ) ;
#12120=EDGE_CURVE ( 'NONE', #74222, #79502, #2109, .T. ) ;
#12162=EDGE_CURVE ( 'NONE', #12424, #61646, #20119, .T. ) ;
#12190=AXIS2_PLACEMENT_3D ( 'NONE', #87312, #80963, #25075 ) ;
#12314=DIRECTION ( 'NONE',  ( 0.000000000000000000, 0.000000000000000000, 1.000000000000000000 ) ) ;
#12355=ORIENTED_EDGE ( 'NONE', *, *, #14313, .F. ) ;
#12381=LINE ( 'NONE', #53682, #50126 ) ;
#12398=CARTESIAN_POINT ( 'NONE',  ( 34.92499999999999716, 82.54999999999999716, 290.4490000000000123 ) ) ;
#12404=AXIS2_PLACEMENT_3D ( 'NONE', #13833, #48777, #77405 ) ;
#12412=CARTESIAN_POINT ( 'NONE',  ( 28.57499999999999929, 77.96728223830730542, 294.9574999999999818 ) ) ;
#12424=VERTEX_POINT ( 'NONE', #57300 ) ;
#12434=VECTOR ( 'NONE', #17400, 1000.000000000000000 ) ;
#12440=DIRECTION ( 'NONE',  ( -0.000000000000000000, -0.000000000000000000, -1.000000000000000000 ) ) ;
#12443=EDGE_CURVE ( 'NONE', #70167, #69623, #42724, .T. ) ;
#12446=VECTOR ( 'NONE', #78464, 1000.000000000000000 ) ;
#12457=DIRECTION ( 'NONE',  ( -0.000000000000000000, -0.000000000000000000, 1.000000000000000000 ) ) ;
#12590=EDGE_LOOP ( 'NONE', ( #79288, #27943, #364, #35638 ) ) ;
#12605=AXIS2_PLACEMENT_3D ( 'NONE', #72892, #45598, #38811 ) ;
#12668=CARTESIAN_POINT ( 'NONE',  ( 47.62500000000000000, 66.67499999999999716, 260.3500000000000227 ) ) ;
#12695=ORIENTED_EDGE ( 'NONE', *, *, #43324, .F. ) ;
#12702=ORIENTED_EDGE ( 'NONE', *, *, #49028, .T. ) ;
#12711=EDGE_LOOP ( 'NONE', ( #1448, #27234, #35622, #26456 ) ) ;
#12729=DIRECTION ( 'NONE',  ( 1.821231995776179916E-16, 0.000000000000000000, 1.000000000000000000 ) ) ;
#12738=VERTEX_POINT ( 'NONE', #68001 ) ;
#12796=CARTESIAN_POINT ( 'NONE',  ( -12.57992038868342810, 81.72639488118660722, 117.8866931554271247 ) ) ;
#12816=CARTESIAN_POINT ( 'NONE',  ( 38.10000000000000142, 82.54999999999999716, 315.3410000000000082 ) ) ;
#12823=DIRECTION ( 'NONE',  ( 0.000000000000000000, -1.000000000000000000, 0.000000000000000000 ) ) ;
#12850=CARTESIAN_POINT ( 'NONE',  ( 47.62500000000000000, 94.53880000000000905, 229.3937500000000114 ) ) ;
#12863=CARTESIAN_POINT ( 'NONE',  ( 44.45000000000000284, 66.67499999999999716, 257.1750000000000114 ) ) ;
#12866=ADVANCED_FACE ( 'NONE', ( #64331 ), #49781, .T. ) ;
#12875=AXIS2_PLACEMENT_3D ( 'NONE', #2897, #66440, #86469 ) ;
#12909=DIRECTION ( 'NONE',  ( 1.000000000000000000, 0.000000000000000000, -9.299908063537909262E-17 ) ) ;
#12974=DIRECTION ( 'NONE',  ( 0.000000000000000000, -1.000000000000000000, 0.000000000000000000 ) ) ;
#12983=CARTESIAN_POINT ( 'NONE',  ( 52.99265158129180264, 69.84999999999999432, 346.9005000000000223 ) ) ;
#13024=DIRECTION ( 'NONE',  ( 0.000000000000000000, -1.000000000000000000, 0.000000000000000000 ) ) ;
#13079=ORIENTED_EDGE ( 'NONE', *, *, #2915, .F. ) ;
#13088=CIRCLE ( 'NONE', #62419, 5.562599999999973122 ) ;
#13149=CARTESIAN_POINT ( 'NONE',  ( 7.778756678762479992E-15, 50.79999999999999716, 222.8849999999999909 ) ) ;
#13176=EDGE_CURVE ( 'NONE', #77621, #67060, #22442, .T. ) ;
#13190=LINE ( 'NONE', #5934, #43055 ) ;
#13192=CARTESIAN_POINT ( 'NONE',  ( 23.71365514520064011, 81.30718046324925297, 307.5032745394355516 ) ) ;
#13230=CARTESIAN_POINT ( 'NONE',  ( 1.523316295016020135E-15, 71.21114727940270939, 265.5569999999999595 ) ) ;
#13254=CARTESIAN_POINT ( 'NONE',  ( 52.99265158129170317, 95.25000000000000000, 358.0130000000000337 ) ) ;
#13260=DIRECTION ( 'NONE',  ( -4.649954031768924432E-17, -0.8660254037844390407, -0.4999999999999995004 ) ) ;
#13273=FACE_OUTER_BOUND ( 'NONE', #43905, .T. ) ;
#13305=DIRECTION ( 'NONE',  ( 0.000000000000000000, 0.000000000000000000, -1.000000000000000000 ) ) ;
#13375=AXIS2_PLACEMENT_3D ( 'NONE', #36601, #35230, #83399 ) ;
#13414=ORIENTED_EDGE ( 'NONE', *, *, #76159, .T. ) ;
#13433=VECTOR ( 'NONE', #12909, 1000.000000000000000 ) ;
#13443=EDGE_LOOP ( 'NONE', ( #17025, #32213, #86020, #87037, #31067 ) ) ;
#13445=DIRECTION ( 'NONE',  ( 0.000000000000000000, 1.000000000000000000, 0.000000000000000000 ) ) ;
#13459=VERTEX_POINT ( 'NONE', #29583 ) ;
#13463=DIRECTION ( 'NONE',  ( 1.748382715945130353E-14, 0.000000000000000000, -1.000000000000000000 ) ) ;
#13578=ORIENTED_EDGE ( 'NONE', *, *, #14395, .T. ) ;
#13608=DIRECTION ( 'NONE',  ( 0.000000000000000000, -1.000000000000000000, 0.000000000000000000 ) ) ;
#13637=ORIENTED_EDGE ( 'NONE', *, *, #72460, .F. ) ;
#13649=DIRECTION ( 'NONE',  ( 1.000000000000000000, 0.000000000000000000, 0.000000000000000000 ) ) ;
#13661=ORIENTED_EDGE ( 'NONE', *, *, #11215, .F. ) ;
#13675=LINE ( 'NONE', #41362, #74047 ) ;
#13699=EDGE_CURVE ( 'NONE', #42802, #3897, #51552, .T. ) ;
#13740=LINE ( 'NONE', #64135, #28716 ) ;
#13750=CARTESIAN_POINT ( 'NONE',  ( -8.621918145265579980, 91.74735363741767458, 118.2424309765198416 ) ) ;
#13833=CARTESIAN_POINT ( 'NONE',  ( 44.45000000000000284, 50.79999999999999716, 257.1750000000000114 ) ) ;
#13842=CARTESIAN_POINT ( 'NONE',  ( 0.000000000000000000, 60.82030000000000314, 265.5569999999999595 ) ) ;
#13868=AXIS2_PLACEMENT_3D ( 'NONE', #2285, #64062, #29989 ) ;
#13886=EDGE_LOOP ( 'NONE', ( #29873, #68371, #76620, #44301 ) ) ;
#13928=AXIS2_PLACEMENT_3D ( 'NONE', #80860, #53997, #79972 ) ;
#13940=ORIENTED_EDGE ( 'NONE', *, *, #59139, .T. ) ;
#13964=CARTESIAN_POINT ( 'NONE',  ( 52.38749999999999574, 94.53880000000000905, 254.7937499999999886 ) ) ;
#13965=ORIENTED_EDGE ( 'NONE', *, *, #50558, .T. ) ;
#14032=VERTEX_POINT ( 'NONE', #11147 ) ;
#14047=AXIS2_PLACEMENT_3D ( 'NONE', #79820, #13445, #6190 ) ;
#14073=DIRECTION ( 'NONE',  ( 0.000000000000000000, -1.000000000000000000, 0.000000000000000000 ) ) ;
#14095=VERTEX_POINT ( 'NONE', #61089 ) ;
#14124=ORIENTED_EDGE ( 'NONE', *, *, #4379, .T. ) ;
#14171=CIRCLE ( 'NONE', #28626, 3.174999999999983391 ) ;
#14200=EDGE_CURVE ( 'NONE', #75737, #77463, #36078, .T. ) ;
#14275=ORIENTED_EDGE ( 'NONE', *, *, #56675, .F. ) ;
#14287=VERTEX_POINT ( 'NONE', #16094 ) ;
#14313=EDGE_CURVE ( 'NONE', #80899, #18726, #82127, .T. ) ;
#14330=ORIENTED_EDGE ( 'NONE', *, *, #41970, .T. ) ;
#14359=FACE_OUTER_BOUND ( 'NONE', #5325, .T. ) ;
#14370=PLANE ( 'NONE',  #83610 ) ;
#14391=ORIENTED_EDGE ( 'NONE', *, *, #38001, .T. ) ;
#14395=EDGE_CURVE ( 'NONE', #1129, #44353, #881, .T. ) ;
#14432=( GEOMETRIC_REPRESENTATION_CONTEXT ( 3 ) GLOBAL_UNCERTAINTY_ASSIGNED_CONTEXT ( ( #68092 ) ) GLOBAL_UNIT_ASSIGNED_CONTEXT ( ( #72782, #38252, #57803 ) ) REPRESENTATION_CONTEXT ( 'NONE', 'WORKASPACE' ) );
#14450=CARTESIAN_POINT ( 'NONE',  ( 7.661254700127844153, 66.45253841614081125, 275.4630000000000223 ) ) ;
#14475=AXIS2_PLACEMENT_3D ( 'NONE', #33802, #26100, #26993 ) ;
#14484=DIRECTION ( 'NONE',  ( -0.000000000000000000, 1.000000000000000000, -0.000000000000000000 ) ) ;
#14497=CARTESIAN_POINT ( 'NONE',  ( 6.812220284937080487E-16, 67.86880000000000734, 271.1195999999999913 ) ) ;
#14512=PLANE ( 'NONE',  #31330 ) ;
#14547=EDGE_LOOP ( 'NONE', ( #2048, #87689, #56691, #27971, #54275 ) ) ;
#14558=CARTESIAN_POINT ( 'NONE',  ( 38.10000000000000142, 69.84999999999999432, 346.9005000000000223 ) ) ;
#14594=CARTESIAN_POINT ( 'NONE',  ( 63.50000000000000000, 66.67499999999999716, 219.0749999999999886 ) ) ;
#14646=CARTESIAN_POINT ( 'NONE',  ( 6.349999999999999645, 82.54999999999999716, 307.6574999999999704 ) ) ;
#14651=DIRECTION ( 'NONE',  ( 1.000000000000000000, 0.000000000000000000, 0.000000000000000000 ) ) ;
#14652=EDGE_LOOP ( 'NONE', ( #51595, #8383, #21193, #70880, #37394 ) ) ;
#14698=LINE ( 'NONE', #69206, #10846 ) ;
#14789=ORIENTED_EDGE ( 'NONE', *, *, #37987, .F. ) ;
#14797=DIRECTION ( 'NONE',  ( 0.000000000000000000, -1.000000000000000000, 0.000000000000000000 ) ) ;
#14934=VECTOR ( 'NONE', #50067, 1000.000000000000000 ) ;
#14984=DIRECTION ( 'NONE',  ( -0.8660254037844387076, 0.4999999999999998890, 0.000000000000000000 ) ) ;
#15012=VECTOR ( 'NONE', #2319, 1000.000000000000000 ) ;
#15033=CARTESIAN_POINT ( 'NONE',  ( -44.45000000000000284, 50.79999999999999716, 257.1750000000000114 ) ) ;
#15064=LINE ( 'NONE', #71381, #24092 ) ;
#15085=EDGE_LOOP ( 'NONE', ( #86110, #30093, #53087, #47246 ) ) ;
#15121=DIRECTION ( 'NONE',  ( 0.000000000000000000, 1.000000000000000000, -0.000000000000000000 ) ) ;
#15123=EDGE_CURVE ( 'NONE', #74222, #44952, #34950, .T. ) ;
#15167=DIRECTION ( 'NONE',  ( 0.000000000000000000, 0.000000000000000000, 1.000000000000000000 ) ) ;
#15188=DIRECTION ( 'NONE',  ( 0.000000000000000000, 0.000000000000000000, -1.000000000000000000 ) ) ;
#15211=DIRECTION ( 'NONE',  ( 0.000000000000000000, -1.000000000000000000, 0.000000000000000000 ) ) ;
#15215=FACE_OUTER_BOUND ( 'NONE', #12590, .T. ) ;
#15217=DIRECTION ( 'NONE',  ( 9.713237310806269221E-16, 0.000000000000000000, -1.000000000000000000 ) ) ;
#15218=ORIENTED_EDGE ( 'NONE', *, *, #56331, .T. ) ;
#15307=PLANE ( 'NONE',  #65428 ) ;
#15313=CARTESIAN_POINT ( 'NONE',  ( 57.14999999999999858, 95.25000000000000000, 297.6879999999999882 ) ) ;
#15362=ADVANCED_FACE ( 'NONE', ( #2690 ), #16760, .F. ) ;
#15373=CARTESIAN_POINT ( 'NONE',  ( 34.92499999999999716, 69.79919999999999902, 346.9005000000000223 ) ) ;
#15374=ORIENTED_EDGE ( 'NONE', *, *, #68578, .F. ) ;
#15424=CARTESIAN_POINT ( 'NONE',  ( 6.938893903907229955E-15, 67.86880000000000734, 216.0269999999999868 ) ) ;
#15433=VERTEX_POINT ( 'NONE', #5820 ) ;
#15437=CARTESIAN_POINT ( 'NONE',  ( 31.75000000000000000, 69.84999999999999432, 295.2750000000000341 ) ) ;
#15474=AXIS2_PLACEMENT_3D ( 'NONE', #6912, #62765, #70042 ) ;
#15488=CARTESIAN_POINT ( 'NONE',  ( 44.45000000000000284, 111.1250000000000000, 257.1750000000000114 ) ) ;
#15517=LINE ( 'NONE', #35486, #42920 ) ;
#15531=CARTESIAN_POINT ( 'NONE',  ( 23.68729270147990462, 84.09221149220967106, 298.3783288177381792 ) ) ;
#15540=EDGE_LOOP ( 'NONE', ( #19777, #4377 ) ) ;
#15579=CARTESIAN_POINT ( 'NONE',  ( 28.57499999999999929, 73.38456447661469895, 302.8950000000000387 ) ) ;
#15580=DIRECTION ( 'NONE',  ( 0.000000000000000000, 1.000000000000000000, 0.000000000000000000 ) ) ;
#15632=ORIENTED_EDGE ( 'NONE', *, *, #58322, .F. ) ;
#15649=LINE ( 'NONE', #16101, #2689 ) ;
#15758=EDGE_CURVE ( 'NONE', #75933, #52977, #86148, .T. ) ;
#15802=CARTESIAN_POINT ( 'NONE',  ( 52.38749999999999574, 94.53880000000000905, 254.7937499999999886 ) ) ;
#15831=ORIENTED_EDGE ( 'NONE', *, *, #25316, .T. ) ;
#15914=DIRECTION ( 'NONE',  ( 0.02992792722492259097, 0.000000000000000000, 0.9995520592605567911 ) ) ;
#15955=EDGE_CURVE ( 'NONE', #68627, #34761, #42770, .T. ) ;
#15965=CARTESIAN_POINT ( 'NONE',  ( 6.938893903907229955E-15, 67.86880000000000734, 216.0269999999999868 ) ) ;
#16039=CARTESIAN_POINT ( 'NONE',  ( 0.000000000000000000, 50.79999999999999716, 265.5569999999999595 ) ) ;
#16093=DIRECTION ( 'NONE',  ( 1.000000000000000000, 0.000000000000000000, 0.000000000000000000 ) ) ;
#16094=CARTESIAN_POINT ( 'NONE',  ( 82.54999999999999716, 95.25000000000000000, 346.9005000000000223 ) ) ;
#16101=CARTESIAN_POINT ( 'NONE',  ( 47.62500000000000000, 66.67499999999999716, 260.3500000000000227 ) ) ;
#16110=VERTEX_POINT ( 'NONE', #10508 ) ;
#16125=VERTEX_POINT ( 'NONE', #29614 ) ;
#16175=CARTESIAN_POINT ( 'NONE',  ( 34.92499999999999716, 66.67499999999999716, 346.0750000000000455 ) ) ;
#16202=DIRECTION ( 'NONE',  ( 0.000000000000000000, 0.000000000000000000, -1.000000000000000000 ) ) ;
#16244=ORIENTED_EDGE ( 'NONE', *, *, #86288, .T. ) ;
#16262=DIRECTION ( 'NONE',  ( 0.000000000000000000, 0.000000000000000000, 1.000000000000000000 ) ) ;
#16307=ORIENTED_EDGE ( 'NONE', *, *, #81098, .T. ) ;
#16329=VECTOR ( 'NONE', #12974, 1000.000000000000000 ) ;
#16388=DIRECTION ( 'NONE',  ( 0.000000000000000000, 1.000000000000000000, 0.000000000000000000 ) ) ;
#16409=EDGE_CURVE ( 'NONE', #21876, #45628, #6822, .T. ) ;
#16419=CARTESIAN_POINT ( 'NONE',  ( 23.74735168769544913, 83.17465673267136594, 307.6189677106137310 ) ) ;
#16424=ORIENTED_EDGE ( 'NONE', *, *, #20016, .T. ) ;
#16486=DIRECTION ( 'NONE',  ( -0.000000000000000000, -0.000000000000000000, -1.000000000000000000 ) ) ;
#16500=EDGE_CURVE ( 'NONE', #42802, #74968, #70862, .T. ) ;
#16528=DIRECTION ( 'NONE',  ( 1.986798540846734824E-16, 0.000000000000000000, -1.000000000000000000 ) ) ;
#16531=CARTESIAN_POINT ( 'NONE',  ( 12.27767421224444533, 79.68862222894867386, 117.9185750741009429 ) ) ;
#16564=AXIS2_PLACEMENT_3D ( 'NONE', #35024, #47299, #510 ) ;
#16567=AXIS2_PLACEMENT_3D ( 'NONE', #78039, #77136, #56206 ) ;
#16614=CARTESIAN_POINT ( 'NONE',  ( 6.938893903907229955E-15, 60.82030000000000314, 209.4690212008904950 ) ) ;
#16694=AXIS2_PLACEMENT_3D ( 'NONE', #35876, #6382, #54946 ) ;
#16711=EDGE_LOOP ( 'NONE', ( #43254, #18882, #69436, #71434, #4625, #62122, #22296, #3354 ) ) ;
#16733=ORIENTED_EDGE ( 'NONE', *, *, #69802, .T. ) ;
#16742=CARTESIAN_POINT ( 'NONE',  ( 38.10000000000000142, 69.84999999999999432, 346.0750000000000455 ) ) ;
#16760=CYLINDRICAL_SURFACE ( 'NONE', #87616, 3.174999999999997158 ) ;
#16761=ORIENTED_EDGE ( 'NONE', *, *, #77263, .F. ) ;
#16789=AXIS2_PLACEMENT_3D ( 'NONE', #11634, #53821, #52039 ) ;
#16822=PLANE ( 'NONE',  #46642 ) ;
#16842=VECTOR ( 'NONE', #49989, 1000.000000000000000 ) ;
#16844=ADVANCED_FACE ( 'NONE', ( #46079 ), #52870, .F. ) ;
#16854=B_SPLINE_CURVE_WITH_KNOTS ( 'NONE', 3,
 ( #75418, #60418, #47683, #13192, #33179, #60877, #88608, #47234, #26364, #54033, #40875, #32725, #81792, #6364, #34055, #73615, #61759, #19545, #88163, #25022, #11393, #11846, #39087, #66798, #4583, #25465, #49017, #22251, #84490, #62670, #48568, #55382, #70390, #77211, #43105, #445 ),
 .UNSPECIFIED., .F., .F.,
 ( 4, 2, 2, 2, 2, 2, 2, 2, 2, 2, 2, 2, 2, 2, 2, 2, 2, 4 ),
 ( 0.01497400908950941197, 0.01590963194845458270, 0.01684525480739975517, 0.01778087766634492417, 0.01871650052529009664, 0.01965212338423526911, 0.02058774624318043811, 0.02152336910212561405, 0.02199118053159819508, 0.02245899196107077611, 0.02339461482001610471, 0.02433023767896143330, 0.02526586053790676190, 0.02620148339685209049, 0.02713710625579741909, 0.02807272911474275115, 0.02900835197368807974, 0.02994397483263340834 ),
 .UNSPECIFIED. ) ;
#16906=ORIENTED_EDGE ( 'NONE', *, *, #60403, .T. ) ;
#16972=LINE ( 'NONE', #44657, #43756 ) ;
#16978=CARTESIAN_POINT ( 'NONE',  ( 12.17775809732705028, 79.28909450904312450, 117.9289698252223815 ) ) ;
#16989=AXIS2_PLACEMENT_3D ( 'NONE', #36920, #27857, #21513 ) ;
#17004=ORIENTED_EDGE ( 'NONE', *, *, #8057, .T. ) ;
#17025=ORIENTED_EDGE ( 'NONE', *, *, #24549, .F. ) ;
#17029=CIRCLE ( 'NONE', #28625, 6.557978799109520196 ) ;
#17095=FACE_OUTER_BOUND ( 'NONE', #15540, .T. ) ;
#17111=DIRECTION ( 'NONE',  ( -0.000000000000000000, -0.000000000000000000, -1.000000000000000000 ) ) ;
#17122=ORIENTED_EDGE ( 'NONE', *, *, #3577, .F. ) ;
#17198=ADVANCED_FACE ( 'NONE', ( #15215 ), #26693, .F. ) ;
#17222=CIRCLE ( 'NONE', #73815, 12.59999999999999964 ) ;
#17230=ORIENTED_EDGE ( 'NONE', *, *, #15123, .F. ) ;
#17258=ORIENTED_EDGE ( 'NONE', *, *, #24105, .T. ) ;
#17311=CARTESIAN_POINT ( 'NONE',  ( 23.58194362415510881, 84.94332446042855622, 307.0240855191376568 ) ) ;
#17394=VECTOR ( 'NONE', #11868, 1000.000000000000000 ) ;
#17400=DIRECTION ( 'NONE',  ( 0.000000000000000000, -1.000000000000000000, 0.000000000000000000 ) ) ;
#17422=CARTESIAN_POINT ( 'NONE',  ( 12.59999999999999964, 82.54999999999999716, 117.8845415480757595 ) ) ;
#17432=CIRCLE ( 'NONE', #52211, 10.26166025953211758 ) ;
#17470=ADVANCED_FACE ( 'NONE', ( #88288 ), #81477, .F. ) ;
#17549=EDGE_LOOP ( 'NONE', ( #75019, #29396, #2763, #8367, #88791 ) ) ;
#17553=CARTESIAN_POINT ( 'NONE',  ( 8.462210198923249696E-15, 71.21114727940270939, 216.0269999999999868 ) ) ;
#17566=CARTESIAN_POINT ( 'NONE',  ( 85.72499999999999432, 66.67499999999999716, 346.0750000000000455 ) ) ;
#17611=ADVANCED_FACE ( 'NONE', ( #51380, #77782 ), #51826, .T. ) ;
#17627=ORIENTED_EDGE ( 'NONE', *, *, #10631, .T. ) ;
#17642=PLANE ( 'NONE',  #40833 ) ;
#17660=CARTESIAN_POINT ( 'NONE',  ( 82.54999999999999716, 69.84999999999999432, 358.0130000000000337 ) ) ;
#17682=AXIS2_PLACEMENT_3D ( 'NONE', #76251, #34906, #62167 ) ;
#17710=ORIENTED_EDGE ( 'NONE', *, *, #23651, .T. ) ;
#17721=CARTESIAN_POINT ( 'NONE',  ( 44.45000000000000284, 111.1250000000000000, 219.0749999999999886 ) ) ;
#17742=VERTEX_POINT ( 'NONE', #25481 ) ;
#17760=ORIENTED_EDGE ( 'NONE', *, *, #25131, .F. ) ;
#17783=CYLINDRICAL_SURFACE ( 'NONE', #31677, 12.44600000000001216 ) ;
#17798=CARTESIAN_POINT ( 'NONE',  ( 44.45000000000000284, 69.84999999999999432, 260.3500000000000227 ) ) ;
#17808=FACE_OUTER_BOUND ( 'NONE', #3589, .T. ) ;
#17829=VERTEX_POINT ( 'NONE', #18221 ) ;
#17866=CARTESIAN_POINT ( 'NONE',  ( 38.10000000000000142, 95.25000000000000000, 346.9005000000000223 ) ) ;
#17900=DIRECTION ( 'NONE',  ( -0.000000000000000000, -0.000000000000000000, -1.000000000000000000 ) ) ;
#17902=ORIENTED_EDGE ( 'NONE', *, *, #16409, .T. ) ;
#17915=DIRECTION ( 'NONE',  ( 0.000000000000000000, 0.000000000000000000, -1.000000000000000000 ) ) ;
#17925=ORIENTED_EDGE ( 'NONE', *, *, #70835, .F. ) ;
#17979=VERTEX_POINT ( 'NONE', #28161 ) ;
#17993=EDGE_CURVE ( 'NONE', #77147, #51227, #55848, .T. ) ;
#18135=PLANE ( 'NONE',  #68611 ) ;
#18146=( GEOMETRIC_REPRESENTATION_CONTEXT ( 3 ) GLOBAL_UNCERTAINTY_ASSIGNED_CONTEXT ( ( #63277 ) ) GLOBAL_UNIT_ASSIGNED_CONTEXT ( ( #42909, #21607, #1612 ) ) REPRESENTATION_CONTEXT ( 'NONE', 'WORKASPACE' ) );
#18150=PRODUCT_CONTEXT ( 'NONE', #35322, 'mechanical' ) ;
#18204=LINE ( 'NONE', #11394, #44710 ) ;
#18221=CARTESIAN_POINT ( 'NONE',  ( 52.99265158129180264, 69.84999999999999432, 358.0130000000000337 ) ) ;
#18235=EDGE_LOOP ( 'NONE', ( #62111, #42683, #87549, #20574 ) ) ;
#18242=DIRECTION ( 'NONE',  ( 0.000000000000000000, -1.000000000000000000, 0.000000000000000000 ) ) ;
#18269=CYLINDRICAL_SURFACE ( 'NONE', #163, 3.174999999999983391 ) ;
#18334=EDGE_LOOP ( 'NONE', ( #47621, #31957, #59427, #72956 ) ) ;
#18403=ADVANCED_FACE ( 'NONE', ( #57093, #805 ), #29865, .T. ) ;
#18404=DIRECTION ( 'NONE',  ( 0.000000000000000000, 0.000000000000000000, 1.000000000000000000 ) ) ;
#18440=EDGE_LOOP ( 'NONE', ( #68546, #74741 ) ) ;
#18472=CARTESIAN_POINT ( 'NONE',  ( 52.38749999999999574, 94.53880000000000905, 250.8250000000000171 ) ) ;
#18544=CARTESIAN_POINT ( 'NONE',  ( 53.97500000000000142, 66.67499999999999716, 209.5499999999999829 ) ) ;
#18552=ORIENTED_EDGE ( 'NONE', *, *, #15123, .T. ) ;
#18661=ORIENTED_EDGE ( 'NONE', *, *, #49475, .F. ) ;
#18681=ORIENTED_EDGE ( 'NONE', *, *, #75951, .F. ) ;
#18695=VERTEX_POINT ( 'NONE', #46133 ) ;
#18698=CARTESIAN_POINT ( 'NONE',  ( -8.321932579531722496, 73.05279115126568001, 118.2650340428489812 ) ) ;
#18726=VERTEX_POINT ( 'NONE', #41565 ) ;
#18762=DIRECTION ( 'NONE',  ( 1.000000000000000000, 0.000000000000000000, -9.299908063537919123E-17 ) ) ;
#18801=VECTOR ( 'NONE', #26541, 999.9999999999998863 ) ;
#18882=ORIENTED_EDGE ( 'NONE', *, *, #11328, .T. ) ;
#18943=PLANE ( 'NONE',  #43431 ) ;
#18982=DIRECTION ( 'NONE',  ( 0.4999999999999998890, 0.8660254037844387076, 0.000000000000000000 ) ) ;
#18990=ORIENTED_EDGE ( 'NONE', *, *, #73779, .T. ) ;
#18998=PLANE ( 'NONE',  #11194 ) ;
#19046=CIRCLE ( 'NONE', #24813, 3.174999999999997158 ) ;
#19049=ORIENTED_EDGE ( 'NONE', *, *, #58787, .T. ) ;
#19063=DIRECTION ( 'NONE',  ( 0.000000000000000000, -1.000000000000000000, 0.000000000000000000 ) ) ;
#19161=( LENGTH_UNIT ( ) NAMED_UNIT ( * ) SI_UNIT ( .MILLI., .METRE. ) );
#19199=VECTOR ( 'NONE', #28058, 1000.000000000000000 ) ;
#19200=DIRECTION ( 'NONE',  ( 3.665114028111779382E-18, -0.9995520592605569021, 0.02992792722492374630 ) ) ;
#19219=CARTESIAN_POINT ( 'NONE',  ( 38.10000000000000142, 82.54999999999999716, 302.8950000000000387 ) ) ;
#19265=DIRECTION ( 'NONE',  ( 0.000000000000000000, 0.000000000000000000, 1.000000000000000000 ) ) ;
#19341=DIRECTION ( 'NONE',  ( -0.000000000000000000, -0.000000000000000000, -1.000000000000000000 ) ) ;
#19345=EDGE_CURVE ( 'NONE', #46288, #14095, #41897, .T. ) ;
#19348=ORIENTED_EDGE ( 'NONE', *, *, #34238, .T. ) ;
#19349=ORIENTED_EDGE ( 'NONE', *, *, #3163, .T. ) ;
#19367=FACE_OUTER_BOUND ( 'NONE', #76430, .T. ) ;
#19382=CARTESIAN_POINT ( 'NONE',  ( 47.62500000000000000, 69.84999999999999432, 288.9250000000000114 ) ) ;
#19442=DIRECTION ( 'NONE',  ( 0.000000000000000000, 0.000000000000000000, -1.000000000000000000 ) ) ;
#19474=LINE ( 'NONE', #47157, #69484 ) ;
#19528=CARTESIAN_POINT ( 'NONE',  ( 31.75000000000000000, 66.67499999999999716, 292.1000000000000227 ) ) ;
#19541=EDGE_CURVE ( 'NONE', #59761, #13459, #19474, .T. ) ;
#19545=CARTESIAN_POINT ( 'NONE',  ( 23.04053976455417185, 77.79540997170535377, 303.2111662390294669 ) ) ;
#19554=EDGE_LOOP ( 'NONE', ( #49125, #22023, #6702, #17230 ) ) ;
#19591=CARTESIAN_POINT ( 'NONE',  ( -12.19523605228628682, 79.27667993837064842, 117.9272132121709689 ) ) ;
#19655=FACE_BOUND ( 'NONE', #78267, .T. ) ;
#19657=AXIS2_PLACEMENT_3D ( 'NONE', #62650, #13608, #425 ) ;
#19687=CARTESIAN_POINT ( 'NONE',  ( 28.57499999999999929, 87.13271776169270311, 294.9574999999999818 ) ) ;
#19702=AXIS2_PLACEMENT_3D ( 'NONE', #38333, #26059, #73298 ) ;
#19744=EDGE_CURVE ( 'NONE', #14095, #70385, #65209, .T. ) ;
#19760=EDGE_CURVE ( 'NONE', #86449, #43505, #79749, .T. ) ;
#19777=ORIENTED_EDGE ( 'NONE', *, *, #82841, .T. ) ;
#19787=CARTESIAN_POINT ( 'NONE',  ( 31.75000000000000000, 66.67499999999999716, 342.8999999999999773 ) ) ;
#19844=EDGE_LOOP ( 'NONE', ( #38656, #35369, #9969, #71080, #39318 ) ) ;
#19873=LINE ( 'NONE', #49353, #3784 ) ;
#19877=CIRCLE ( 'NONE', #30061, 12.44600000000001216 ) ;
#19920=CARTESIAN_POINT ( 'NONE',  ( 44.45000000000000284, 66.67499999999999716, 219.0749999999999886 ) ) ;
#19964=DIRECTION ( 'NONE',  ( 0.000000000000000000, 0.000000000000000000, -1.000000000000000000 ) ) ;
#20005=AXIS2_PLACEMENT_3D ( 'NONE', #48223, #89144, #33277 ) ;
#20016=EDGE_CURVE ( 'NONE', #45281, #65225, #80714, .T. ) ;
#20045=VERTEX_POINT ( 'NONE', #86631 ) ;
#20050=CARTESIAN_POINT ( 'NONE',  ( 57.14999999999999858, 69.84999999999999432, 300.8629999999999995 ) ) ;
#20051=VECTOR ( 'NONE', #5861, 1000.000000000000000 ) ;
#20079=FACE_OUTER_BOUND ( 'NONE', #65388, .T. ) ;
#20119=LINE ( 'NONE', #12863, #84796 ) ;
#20243=AXIS2_PLACEMENT_3D ( 'NONE', #37961, #45205, #23019 ) ;
#20289=CARTESIAN_POINT ( 'NONE',  ( 47.62500000000000000, 66.67499999999999716, 257.1750000000000114 ) ) ;
#20331=CARTESIAN_POINT ( 'NONE',  ( 0.000000000000000000, 67.86880000000000734, 259.9944000000000415 ) ) ;
#20383=DIRECTION ( 'NONE',  ( -0.000000000000000000, -0.000000000000000000, -1.000000000000000000 ) ) ;
#20415=DIRECTION ( 'NONE',  ( -0.000000000000000000, 1.000000000000000000, 0.000000000000000000 ) ) ;
#20417=EDGE_CURVE ( 'NONE', #22058, #89758, #80163, .T. ) ;
#20452=DIRECTION ( 'NONE',  ( 0.000000000000000000, 0.000000000000000000, -1.000000000000000000 ) ) ;
#20469=ORIENTED_EDGE ( 'NONE', *, *, #88184, .F. ) ;
#20470=AXIS2_PLACEMENT_3D ( 'NONE', #54164, #81924, #38325 ) ;
#20480=ORIENTED_EDGE ( 'NONE', *, *, #72583, .F. ) ;
#20563=AXIS2_PLACEMENT_3D ( 'NONE', #48003, #88924, #75740 ) ;
#20574=ORIENTED_EDGE ( 'NONE', *, *, #39026, .T. ) ;
#20577=CARTESIAN_POINT ( 'NONE',  ( -12.60000000000000497, 83.37282639406460305, 117.8845415480758021 ) ) ;
#20592=DIRECTION ( 'NONE',  ( 1.000000000000000000, 0.000000000000000000, -9.299908063537909262E-17 ) ) ;
#20600=ORIENTED_EDGE ( 'NONE', *, *, #76617, .F. ) ;
#20620=AXIS2_PLACEMENT_3D ( 'NONE', #2130, #38413, #45652 ) ;
#20640=CIRCLE ( 'NONE', #48165, 3.174999999999983391 ) ;
#20693=ORIENTED_EDGE ( 'NONE', *, *, #65049, .T. ) ;
#20781=ORIENTED_EDGE ( 'NONE', *, *, #6337, .T. ) ;
#20926=ORIENTED_EDGE ( 'NONE', *, *, #46869, .F. ) ;
#20935=FACE_BOUND ( 'NONE', #62365, .T. ) ;
#20960=CARTESIAN_POINT ( 'NONE',  ( 53.97500000000000142, 95.25000000000000000, 283.4005000000000223 ) ) ;
#20962=DIRECTION ( 'NONE',  ( -1.000000000000000000, 0.000000000000000000, 0.000000000000000000 ) ) ;
#20983=DIRECTION ( 'NONE',  ( 0.000000000000000000, 0.000000000000000000, -1.000000000000000000 ) ) ;
#20986=EDGE_LOOP ( 'NONE', ( #21669, #76286, #23296, #57582 ) ) ;
#21003=DIRECTION ( 'NONE',  ( -1.000000000000000000, 0.000000000000000000, 0.000000000000000000 ) ) ;
#21035=CIRCLE ( 'NONE', #25436, 3.174999999999983391 ) ;
#21056=CIRCLE ( 'NONE', #3607, 3.174999999999983391 ) ;
#21113=EDGE_LOOP ( 'NONE', ( #62877, #63981, #18552, #20693 ) ) ;
#21171=DIRECTION ( 'NONE',  ( -1.000000000000000000, 0.000000000000000000, -1.748382715945130353E-14 ) ) ;
#21193=ORIENTED_EDGE ( 'NONE', *, *, #19744, .F. ) ;
#21194=DIRECTION ( 'NONE',  ( 0.000000000000000000, 0.000000000000000000, -1.000000000000000000 ) ) ;
#21208=ORIENTED_EDGE ( 'NONE', *, *, #23044, .T. ) ;
#21216=DIRECTION ( 'NONE',  ( 0.000000000000000000, -0.000000000000000000, -1.000000000000000000 ) ) ;
#21228=AXIS2_PLACEMENT_3D ( 'NONE', #65998, #3790, #58304 ) ;
#21244=ORIENTED_EDGE ( 'NONE', *, *, #79068, .T. ) ;
#21262=DIRECTION ( 'NONE',  ( 0.000000000000000000, 0.000000000000000000, 1.000000000000000000 ) ) ;
#21264=CARTESIAN_POINT ( 'NONE',  ( 12.60000000000000142, 83.38255235285211597, 117.8845415480757595 ) ) ;
#21280=ADVANCED_FACE ( 'NONE', ( #10621 ), #32852, .F. ) ;
#21281=DIRECTION ( 'NONE',  ( 1.000000000000000000, 0.000000000000000000, 0.000000000000000000 ) ) ;
#21298=DIRECTION ( 'NONE',  ( 3.665114028111779382E-18, -0.9995520592605569021, 0.02992792722492374630 ) ) ;
#21363=LINE ( 'NONE', #49037, #39044 ) ;
#21376=ORIENTED_EDGE ( 'NONE', *, *, #50501, .F. ) ;
#21387=ORIENTED_EDGE ( 'NONE', *, *, #80871, .T. ) ;
#21406=ADVANCED_FACE ( 'NONE', ( #40565 ), #48701, .F. ) ;
#21419=CARTESIAN_POINT ( 'NONE',  ( 85.72499999999999432, 66.67499999999999716, 342.8999999999999773 ) ) ;
#21422=CONICAL_SURFACE ( 'NONE', #24338, 10.66800000000000459, 0.02993239667170383839 ) ;
#21436=AXIS2_PLACEMENT_3D ( 'NONE', #70310, #71222, #8086 ) ;
#21498=ORIENTED_EDGE ( 'NONE', *, *, #26510, .T. ) ;
#21513=DIRECTION ( 'NONE',  ( 0.000000000000000000, -1.000000000000000000, 0.000000000000000000 ) ) ;
#21517=CARTESIAN_POINT ( 'NONE',  ( -12.59999999999999964, 82.54999999999999716, 206.3750000000000000 ) ) ;
#21562=CARTESIAN_POINT ( 'NONE',  ( 0.000000000000000000, 60.82030000000000314, 265.5569999999999595 ) ) ;
#21570=VECTOR ( 'NONE', #49229, 1000.000000000000000 ) ;
#21607=( NAMED_UNIT ( * ) PLANE_ANGLE_UNIT ( ) SI_UNIT ( $, .RADIAN. ) );
#21650=FACE_OUTER_BOUND ( 'NONE', #6581, .T. ) ;
#21669=ORIENTED_EDGE ( 'NONE', *, *, #87288, .T. ) ;
#21686=AXIS2_PLACEMENT_3D ( 'NONE', #22253, #14984, #29506 ) ;
#21709=ADVANCED_FACE ( 'NONE', ( #32748 ), #17783, .T. ) ;
#21714=EDGE_CURVE ( 'NONE', #78417, #75698, #88240, .T. ) ;
#21724=CARTESIAN_POINT ( 'NONE',  ( 12.59999999999999964, 82.54999999999999716, 117.8845415480757595 ) ) ;
#21727=CARTESIAN_POINT ( 'NONE',  ( -7.661254700127833495, 82.54999999999999716, 317.6630000000000109 ) ) ;
#21745=ORIENTED_EDGE ( 'NONE', *, *, #81339, .T. ) ;
#21755=EDGE_LOOP ( 'NONE', ( #55841, #42288, #81367, #3152 ) ) ;
#21793=EDGE_LOOP ( 'NONE', ( #15374, #13661, #27751, #58767 ) ) ;
#21845=ORIENTED_EDGE ( 'NONE', *, *, #53593, .F. ) ;
#21849=EDGE_CURVE ( 'NONE', #11575, #2492, #83905, .T. ) ;
#21876=VERTEX_POINT ( 'NONE', #47706 ) ;
#21902=CARTESIAN_POINT ( 'NONE',  ( 7.661254700127833495, 82.54999999999999716, 320.6630000000000109 ) ) ;
#21950=CARTESIAN_POINT ( 'NONE',  ( 88.90000000000000568, 66.67499999999999716, 219.0749999999999886 ) ) ;
#21962=DIRECTION ( 'NONE',  ( 0.000000000000000000, 0.000000000000000000, -1.000000000000000000 ) ) ;
#21979=ORIENTED_EDGE ( 'NONE', *, *, #13176, .F. ) ;
#21996=DIRECTION ( 'NONE',  ( 1.000000000000000000, 0.000000000000000000, 0.000000000000000000 ) ) ;
#22010=PLANE ( 'NONE',  #12404 ) ;
#22023=ORIENTED_EDGE ( 'NONE', *, *, #53206, .T. ) ;
#22058=VERTEX_POINT ( 'NONE', #80366 ) ;
#22082=CARTESIAN_POINT ( 'NONE',  ( 47.62500000000000000, 111.1250000000000000, 257.1750000000000114 ) ) ;
#22094=CARTESIAN_POINT ( 'NONE',  ( 44.45000000000000284, 50.79999999999999716, 206.3750000000000000 ) ) ;
#22177=CARTESIAN_POINT ( 'NONE',  ( 11.65427314393061309, 87.39163397251130050, 117.9821062356120080 ) ) ;
#22211=FACE_BOUND ( 'NONE', #81715, .T. ) ;
#22225=FACE_BOUND ( 'NONE', #89735, .T. ) ;
#22237=DIRECTION ( 'NONE',  ( 0.000000000000000000, 0.000000000000000000, -1.000000000000000000 ) ) ;
#22251=CARTESIAN_POINT ( 'NONE',  ( 23.44892695906009905, 79.39921112727093089, 299.3104155498348291 ) ) ;
#22253=CARTESIAN_POINT ( 'NONE',  ( 52.99265158129170317, 95.25000000000000000, 346.9005000000000223 ) ) ;
#22264=ORIENTED_EDGE ( 'NONE', *, *, #68550, .T. ) ;
#22296=ORIENTED_EDGE ( 'NONE', *, *, #54344, .T. ) ;
#22301=ORIENTED_EDGE ( 'NONE', *, *, #77802, .F. ) ;
#22311=FACE_OUTER_BOUND ( 'NONE', #74906, .T. ) ;
#22341=CARTESIAN_POINT ( 'NONE',  ( 23.71390425477495256, 83.78871496225653459, 298.2858669080578693 ) ) ;
#22346=FACE_OUTER_BOUND ( 'NONE', #84073, .T. ) ;
#22354=ORIENTED_EDGE ( 'NONE', *, *, #64174, .T. ) ;
#22357=DIRECTION ( 'NONE',  ( 0.000000000000000000, -0.9995520592605569021, -0.02992792722492374630 ) ) ;
#22365=ORIENTED_EDGE ( 'NONE', *, *, #7301, .F. ) ;
#22382=AXIS2_PLACEMENT_3D ( 'NONE', #17798, #18242, #81396 ) ;
#22442=LINE ( 'NONE', #60053, #77638 ) ;
#22464=CARTESIAN_POINT ( 'NONE',  ( 6.812220284937059779E-16, 60.82030000000000314, 271.1195999999999913 ) ) ;
#22479=AXIS2_PLACEMENT_3D ( 'NONE', #22784, #37745, #72712 ) ;
#22537=LINE ( 'NONE', #37048, #76780 ) ;
#22601=TOROIDAL_SURFACE ( 'NONE', #61731, 13.09746158385919124, 3.000000000000000000 ) ;
#22619=CARTESIAN_POINT ( 'NONE',  ( 9.487327754115383982, 90.88213376798057652, 118.1772177615633126 ) ) ;
#22630=CARTESIAN_POINT ( 'NONE',  ( 38.10000000000000142, 82.54999999999999716, 302.8950000000000387 ) ) ;
#22747=EDGE_CURVE ( 'NONE', #81285, #89072, #56434, .T. ) ;
#22784=CARTESIAN_POINT ( 'NONE',  ( 44.45000000000000284, 66.67499999999999716, 219.0749999999999886 ) ) ;
#22808=DIRECTION ( 'NONE',  ( 0.000000000000000000, 1.000000000000000000, 0.000000000000000000 ) ) ;
#22868=EDGE_CURVE ( 'NONE', #16110, #40366, #74564, .T. ) ;
#22911=CARTESIAN_POINT ( 'NONE',  ( 0.8226717696920563538, 69.95000000000000284, 118.5560000000000258 ) ) ;
#22960=EDGE_CURVE ( 'NONE', #67060, #22058, #30092, .T. ) ;
#23019=DIRECTION ( 'NONE',  ( -1.821231995776174246E-16, 0.000000000000000000, -1.000000000000000000 ) ) ;
#23044=EDGE_CURVE ( 'NONE', #61646, #49324, #77501, .T. ) ;
#23076=VECTOR ( 'NONE', #74793, 1000.000000000000000 ) ;
#23126=EDGE_LOOP ( 'NONE', ( #72073, #33021 ) ) ;
#23177=ORIENTED_EDGE ( 'NONE', *, *, #33739, .F. ) ;
#23229=CARTESIAN_POINT ( 'NONE',  ( 51.39690000000000225, 82.54999999999999716, 358.0130000000000337 ) ) ;
#23256=CARTESIAN_POINT ( 'NONE',  ( 23.35554434807808022, 86.13711066444062681, 299.7470812929934709 ) ) ;
#23296=ORIENTED_EDGE ( 'NONE', *, *, #64892, .T. ) ;
#23340=ORIENTED_EDGE ( 'NONE', *, *, #20417, .F. ) ;
#23377=LINE ( 'NONE', #17866, #53708 ) ;
#23386=VERTEX_POINT ( 'NONE', #25401 ) ;
#23411=CARTESIAN_POINT ( 'NONE',  ( 44.45000000000000284, 66.67499999999999716, 288.9250000000000114 ) ) ;
#23477=DIRECTION ( 'NONE',  ( 0.8660254037844387076, 0.4999999999999998890, 0.000000000000000000 ) ) ;
#23480=CYLINDRICAL_SURFACE ( 'NONE', #20620, 118.5560000000000116 ) ;
#23521=ORIENTED_EDGE ( 'NONE', *, *, #19541, .T. ) ;
#23651=EDGE_CURVE ( 'NONE', #75721, #68410, #81911, .T. ) ;
#23659=EDGE_CURVE ( 'NONE', #79502, #74222, #63014, .T. ) ;
#23662=LINE ( 'NONE', #79970, #15012 ) ;
#23665=ADVANCED_FACE ( 'NONE', ( #64850 ), #83967, .T. ) ;
#23696=EDGE_LOOP ( 'NONE', ( #58960, #75618, #52195 ) ) ;
#23744=ADVANCED_FACE ( 'NONE', ( #57577 ), #50768, .T. ) ;
#23753=DIRECTION ( 'NONE',  ( 1.049727191138617833E-16, -0.5150380749100549327, 0.8571673007021118895 ) ) ;
#23803=CARTESIAN_POINT ( 'NONE',  ( 11.79654850775738240, 78.10342437589451947, 117.9677577584307926 ) ) ;
#23805=ORIENTED_EDGE ( 'NONE', *, *, #2347, .T. ) ;
#23814=VECTOR ( 'NONE', #61911, 1000.000000000000000 ) ;
#23825=ORIENTED_EDGE ( 'NONE', *, *, #30218, .F. ) ;
#23965=DIRECTION ( 'NONE',  ( 0.000000000000000000, 0.000000000000000000, -1.000000000000000000 ) ) ;
#23966=EDGE_CURVE ( 'NONE', #70579, #85819, #76587, .T. ) ;
#23990=ADVANCED_FACE ( 'NONE', ( #41147 ), #82968, .F. ) ;
#23994=DIRECTION ( 'NONE',  ( 1.000000000000000000, 0.000000000000000000, 0.000000000000000000 ) ) ;
#24079=CARTESIAN_POINT ( 'NONE',  ( 74.98969683741650272, 82.54999999999999716, 358.0130000000000337 ) ) ;
#24092=VECTOR ( 'NONE', #77288, 1000.000000000000000 ) ;
#24104=LINE ( 'NONE', #85001, #16842 ) ;
#24105=EDGE_CURVE ( 'NONE', #1814, #74222, #34339, .T. ) ;
#24113=DIRECTION ( 'NONE',  ( 0.000000000000000000, 0.000000000000000000, -1.000000000000000000 ) ) ;
#24114=ORIENTED_EDGE ( 'NONE', *, *, #75119, .F. ) ;
#24126=CARTESIAN_POINT ( 'NONE',  ( 23.30833798207798324, 86.33530863199757732, 305.8016272809862812 ) ) ;
#24183=CARTESIAN_POINT ( 'NONE',  ( 7.661254700127822836, 98.64746158385918307, 317.6630000000000109 ) ) ;
#24216=ORIENTED_EDGE ( 'NONE', *, *, #36466, .F. ) ;
#24272=CIRCLE ( 'NONE', #75035, 16.09746158385918946 ) ;
#24277=CYLINDRICAL_SURFACE ( 'NONE', #19702, 12.59999999999999964 ) ;
#24338=AXIS2_PLACEMENT_3D ( 'NONE', #45731, #52099, #23994 ) ;
#24359=AXIS2_PLACEMENT_3D ( 'NONE', #34142, #61840, #1439 ) ;
#24379=VERTEX_POINT ( 'NONE', #33790 ) ;
#24400=VECTOR ( 'NONE', #31324, 1000.000000000000000 ) ;
#24468=DIRECTION ( 'NONE',  ( -1.000000000000000000, 0.000000000000000000, 0.000000000000000000 ) ) ;
#24526=CARTESIAN_POINT ( 'NONE',  ( 44.45000000000000284, 111.1250000000000000, 219.0749999999999886 ) ) ;
#24549=EDGE_CURVE ( 'NONE', #69843, #75721, #46503, .T. ) ;
#24620=CARTESIAN_POINT ( 'NONE',  ( -0.8234102327917739439, 69.97007251634678937, 118.5538614604470098 ) ) ;
#24700=EDGE_CURVE ( 'NONE', #9455, #27014, #87653, .T. ) ;
#24796=FACE_OUTER_BOUND ( 'NONE', #26942, .T. ) ;
#24813=AXIS2_PLACEMENT_3D ( 'NONE', #29171, #35070, #76873 ) ;
#24893=EDGE_CURVE ( 'NONE', #1197, #86595, #76766, .T. ) ;
#24909=CARTESIAN_POINT ( 'NONE',  ( 34.92499999999999716, 69.84999999999999432, 346.0750000000000455 ) ) ;
#24926=DIRECTION ( 'NONE',  ( -1.000000000000000000, 0.000000000000000000, 1.821231995776179916E-16 ) ) ;
#24927=ORIENTED_EDGE ( 'NONE', *, *, #68387, .T. ) ;
#24959=FACE_BOUND ( 'NONE', #58654, .T. ) ;
#24977=EDGE_CURVE ( 'NONE', #14032, #79692, #55929, .T. ) ;
#24987=CARTESIAN_POINT ( 'NONE',  ( 6.938893903907229955E-15, 60.82030000000000314, 216.0269999999999868 ) ) ;
#24988=LINE ( 'NONE', #34018, #87748 ) ;
#24990=VERTEX_POINT ( 'NONE', #12983 ) ;
#25001=CARTESIAN_POINT ( 'NONE',  ( 28.57499999999999929, 87.13271776169270311, 294.9574999999999818 ) ) ;
#25009=CARTESIAN_POINT ( 'NONE',  ( 34.92499999999999716, 69.79919999999999902, 346.9005000000000223 ) ) ;
#25022=CARTESIAN_POINT ( 'NONE',  ( 23.03807392221892769, 77.78746915432593312, 302.5815555703470068 ) ) ;
#25075=DIRECTION ( 'NONE',  ( -1.000000000000000000, -5.369304423922379141E-17, 0.000000000000000000 ) ) ;
#25086=VECTOR ( 'NONE', #28991, 1000.000000000000000 ) ;
#25100=EDGE_CURVE ( 'NONE', #60387, #47202, #4375, .T. ) ;
#25131=EDGE_CURVE ( 'NONE', #14095, #69623, #68391, .T. ) ;
#25145=ORIENTED_EDGE ( 'NONE', *, *, #85183, .F. ) ;
#25182=ADVANCED_FACE ( 'NONE', ( #45136 ), #24277, .T. ) ;
#25197=EDGE_LOOP ( 'NONE', ( #41750, #81629, #47526, #14391 ) ) ;
#25229=DIRECTION ( 'NONE',  ( 0.000000000000000000, 0.000000000000000000, -1.000000000000000000 ) ) ;
#25249=ORIENTED_EDGE ( 'NONE', *, *, #55807, .T. ) ;
#25289=DIRECTION ( 'NONE',  ( 1.000000000000000000, -0.000000000000000000, 0.000000000000000000 ) ) ;
#25307=EDGE_LOOP ( 'NONE', ( #31365, #17122, #11546, #83026 ) ) ;
#25316=EDGE_CURVE ( 'NONE', #86595, #18695, #62797, .T. ) ;
#25331=LINE ( 'NONE', #73939, #55886 ) ;
#25334=FACE_OUTER_BOUND ( 'NONE', #85876, .T. ) ;
#25401=CARTESIAN_POINT ( 'NONE',  ( 88.90000000000000568, 69.84999999999999432, 244.4749999999999943 ) ) ;
#25436=AXIS2_PLACEMENT_3D ( 'NONE', #61166, #27990, #55226 ) ;
#25441=DIRECTION ( 'NONE',  ( 0.000000000000000000, -1.000000000000000000, 0.000000000000000000 ) ) ;
#25464=LINE ( 'NONE', #74061, #64799 ) ;
#25465=CARTESIAN_POINT ( 'NONE',  ( 23.30868458379111985, 78.76602235523037621, 299.9862232315379629 ) ) ;
#25474=ORIENTED_EDGE ( 'NONE', *, *, #7573, .F. ) ;
#25481=CARTESIAN_POINT ( 'NONE',  ( 0.000000000000000000, 60.82030000000000314, 258.9990212008905246 ) ) ;
#25492=VECTOR ( 'NONE', #9147, 1000.000000000000000 ) ;
#25498=DIRECTION ( 'NONE',  ( 0.8660254037844387076, -0.4999999999999998890, 0.000000000000000000 ) ) ;
#25505=ORIENTED_EDGE ( 'NONE', *, *, #7917, .F. ) ;
#25513=VECTOR ( 'NONE', #12440, 1000.000000000000000 ) ;
#25519=DIRECTION ( 'NONE',  ( 1.000000000000000000, 0.000000000000000000, 0.000000000000000000 ) ) ;
#25535=ORIENTED_EDGE ( 'NONE', *, *, #77772, .T. ) ;
#25549=EDGE_LOOP ( 'NONE', ( #76585, #76503, #33187, #70342 ) ) ;
#25626=CARTESIAN_POINT ( 'NONE',  ( 31.75000000000000000, 66.67499999999999716, 346.0750000000000455 ) ) ;
#25631=CARTESIAN_POINT ( 'NONE',  ( 31.75000000000000000, 66.67499999999999716, 342.8999999999999773 ) ) ;
#25643=LINE ( 'NONE', #54661, #83475 ) ;
#25662=ORIENTED_EDGE ( 'NONE', *, *, #85909, .T. ) ;
#25671=DIRECTION ( 'NONE',  ( -1.000000000000000000, 0.000000000000000000, 0.000000000000000000 ) ) ;
#25732=LINE ( 'NONE', #82959, #8511 ) ;
#25738=CARTESIAN_POINT ( 'NONE',  ( 7.661254700127844153, 69.45253841614081125, 320.6630000000000109 ) ) ;
#25741=CARTESIAN_POINT ( 'NONE',  ( 0.000000000000000000, 82.54999999999999716, 206.3750000000000000 ) ) ;
#25763=CIRCLE ( 'NONE', #21436, 3.000000000000002665 ) ;
#25769=ORIENTED_EDGE ( 'NONE', *, *, #34238, .F. ) ;
#25800=CARTESIAN_POINT ( 'NONE',  ( 50.79999999999999716, 73.02500000000000568, 257.1750000000000114 ) ) ;
#25815=LINE ( 'NONE', #11283, #67702 ) ;
#25823=AXIS2_PLACEMENT_3D ( 'NONE', #52686, #61319, #74514 ) ;
#25906=FACE_OUTER_BOUND ( 'NONE', #14547, .T. ) ;
#25955=DIRECTION ( 'NONE',  ( 0.000000000000000000, 0.000000000000000000, -1.000000000000000000 ) ) ;
#25968=CARTESIAN_POINT ( 'NONE',  ( -10.70251298044785493, 75.88783213464688515, 118.0721548101077474 ) ) ;
#25990=EDGE_CURVE ( 'NONE', #2492, #14095, #2729, .T. ) ;
#25998=EDGE_CURVE ( 'NONE', #84598, #35448, #70427, .T. ) ;
#26025=STYLED_ITEM ( 'NONE', ( #5992 ), #44568 ) ;
#26033=PLANE ( 'NONE',  #51891 ) ;
#26042=CARTESIAN_POINT ( 'NONE',  ( -5.590575964937773534, 93.87199967727632099, 118.4265748443029338 ) ) ;
#26053=ORIENTED_EDGE ( 'NONE', *, *, #68578, .T. ) ;
#26059=DIRECTION ( 'NONE',  ( -0.000000000000000000, -0.000000000000000000, 1.000000000000000000 ) ) ;
#26100=DIRECTION ( 'NONE',  ( 0.000000000000000000, 0.000000000000000000, 1.000000000000000000 ) ) ;
#26101=DIRECTION ( 'NONE',  ( 0.000000000000000000, 1.000000000000000000, 0.000000000000000000 ) ) ;
#26119=DIRECTION ( 'NONE',  ( 0.000000000000000000, 0.000000000000000000, -1.000000000000000000 ) ) ;
#26125=LINE ( 'NONE', #39734, #63176 ) ;
#26153=AXIS2_PLACEMENT_3D ( 'NONE', #39477, #33113, #61258 ) ;
#26195=CIRCLE ( 'NONE', #45041, 5.562600000000000655 ) ;
#26202=FACE_OUTER_BOUND ( 'NONE', #25307, .T. ) ;
#26342=FACE_OUTER_BOUND ( 'NONE', #23696, .T. ) ;
#26364=CARTESIAN_POINT ( 'NONE',  ( 23.44962858617382295, 79.40261884150201865, 306.4827471306458051 ) ) ;
#26416=DIRECTION ( 'NONE',  ( -0.000000000000000000, 1.000000000000000000, 0.000000000000000000 ) ) ;
#26424=CARTESIAN_POINT ( 'NONE',  ( 34.92499999999999716, 66.67499999999999716, 295.2750000000000341 ) ) ;
#26430=CARTESIAN_POINT ( 'NONE',  ( 88.90000000000000568, 66.67499999999999716, 219.0749999999999886 ) ) ;
#26456=ORIENTED_EDGE ( 'NONE', *, *, #76350, .T. ) ;
#26510=EDGE_CURVE ( 'NONE', #70068, #1129, #72003, .T. ) ;
#26541=DIRECTION ( 'NONE',  ( 0.000000000000000000, 0.4999999999999995004, -0.8660254037844390407 ) ) ;
#26545=ORIENTED_EDGE ( 'NONE', *, *, #77466, .F. ) ;
#26577=CARTESIAN_POINT ( 'NONE',  ( 38.10000000000000142, 69.84999999999999432, 346.9005000000000223 ) ) ;
#26583=CARTESIAN_POINT ( 'NONE',  ( 49.65699999999999648, 82.54999999999999716, 358.0130000000000337 ) ) ;
#26683=CARTESIAN_POINT ( 'NONE',  ( 57.14999999999999858, 95.25000000000000000, 280.2255000000000109 ) ) ;
#26693=CYLINDRICAL_SURFACE ( 'NONE', #73039, 3.174999999999983391 ) ;
#26699=AXIS2_PLACEMENT_3D ( 'NONE', #41020, #68742, #78265 ) ;
#26700=EDGE_LOOP ( 'NONE', ( #80219, #15632, #62351, #71980 ) ) ;
#26718=CARTESIAN_POINT ( 'NONE',  ( 34.92499999999999716, 73.38456447661469895, 302.8950000000000387 ) ) ;
#26801=DIRECTION ( 'NONE',  ( 0.000000000000000000, 1.000000000000000000, 6.056575390184510167E-15 ) ) ;
#26832=ORIENTED_EDGE ( 'NONE', *, *, #19541, .F. ) ;
#26835=VECTOR ( 'NONE', #67519, 999.9999999999998863 ) ;
#26851=CARTESIAN_POINT ( 'NONE',  ( -6.662630065772598975, 71.84777277514653804, 118.3691311527337859 ) ) ;
#26860=SURFACE_STYLE_FILL_AREA ( #32319 ) ;
#26862=DIRECTION ( 'NONE',  ( 0.000000000000000000, 0.000000000000000000, 1.000000000000000000 ) ) ;
#26871=LINE ( 'NONE', #13254, #41183 ) ;
#26876=CARTESIAN_POINT ( 'NONE',  ( 28.57499999999999929, 91.71543552338529537, 302.8950000000000387 ) ) ;
#26879=AXIS2_PLACEMENT_3D ( 'NONE', #16039, #41918, #28296 ) ;
#26942=EDGE_LOOP ( 'NONE', ( #32719, #11617, #60551 ) ) ;
#26993=DIRECTION ( 'NONE',  ( 1.000000000000000000, 0.000000000000000000, 0.000000000000000000 ) ) ;
#27014=VERTEX_POINT ( 'NONE', #24183 ) ;
#27048=EDGE_CURVE ( 'NONE', #37074, #28060, #69720, .T. ) ;
#27074=EDGE_CURVE ( 'NONE', #40366, #34574, #54976, .T. ) ;
#27084=CARTESIAN_POINT ( 'NONE',  ( 28.57499999999999929, 82.54999999999999716, 302.8950000000000387 ) ) ;
#27107=AXIS2_PLACEMENT_3D ( 'NONE', #88989, #14484, #54428 ) ;
#27121=ORIENTED_EDGE ( 'NONE', *, *, #70304, .T. ) ;
#27173=EDGE_CURVE ( 'NONE', #59761, #30868, #13675, .T. ) ;
#27219=DIRECTION ( 'NONE',  ( 0.000000000000000000, 0.000000000000000000, 1.000000000000000000 ) ) ;
#27231=EDGE_CURVE ( 'NONE', #58613, #41326, #39225, .T. ) ;
#27232=AXIS2_PLACEMENT_3D ( 'NONE', #31861, #80938, #5521 ) ;
#27234=ORIENTED_EDGE ( 'NONE', *, *, #46201, .F. ) ;
#27284=VERTEX_POINT ( 'NONE', #44501 ) ;
#27295=CARTESIAN_POINT ( 'NONE',  ( 7.661254700127844153, 66.45253841614081125, 275.4630000000000223 ) ) ;
#27302=CARTESIAN_POINT ( 'NONE',  ( -4.059050453778890066, 70.59316187249579855, 118.4889539811882457 ) ) ;
#27352=FACE_OUTER_BOUND ( 'NONE', #71068, .T. ) ;
#27468=ORIENTED_EDGE ( 'NONE', *, *, #42615, .F. ) ;
#27509=EDGE_LOOP ( 'NONE', ( #57301, #82291, #55633, #47866 ) ) ;
#27527=DIRECTION ( 'NONE',  ( 0.000000000000000000, 0.000000000000000000, -1.000000000000000000 ) ) ;
#27568=ORIENTED_EDGE ( 'NONE', *, *, #72395, .T. ) ;
#27617=CARTESIAN_POINT ( 'NONE',  ( 51.39690000000000225, 82.54999999999999716, 335.3740053999999304 ) ) ;
#27751=ORIENTED_EDGE ( 'NONE', *, *, #28319, .F. ) ;
#27784=LINE ( 'NONE', #77743, #25492 ) ;
#27786=DIRECTION ( 'NONE',  ( 0.000000000000000000, -1.000000000000000000, 0.000000000000000000 ) ) ;
#27797=CARTESIAN_POINT ( 'NONE',  ( 23.75871628398702384, 82.54999999999999716, 298.1325000000000500 ) ) ;
#27816=EDGE_CURVE ( 'NONE', #51066, #44952, #63945, .T. ) ;
#27857=DIRECTION ( 'NONE',  ( 0.000000000000000000, 0.000000000000000000, -1.000000000000000000 ) ) ;
#27922=EDGE_CURVE ( 'NONE', #1768, #79680, #29000, .T. ) ;
#27943=ORIENTED_EDGE ( 'NONE', *, *, #48563, .F. ) ;
#27971=ORIENTED_EDGE ( 'NONE', *, *, #59207, .T. ) ;
#27990=DIRECTION ( 'NONE',  ( 0.000000000000000000, 1.000000000000000000, 0.000000000000000000 ) ) ;
#27992=CARTESIAN_POINT ( 'NONE',  ( 53.97500000000000142, 69.84999999999999432, 283.4005000000000223 ) ) ;
#28058=DIRECTION ( 'NONE',  ( 0.000000000000000000, 1.000000000000000000, 0.000000000000000000 ) ) ;
#28060=VERTEX_POINT ( 'NONE', #47962 ) ;
#28066=VECTOR ( 'NONE', #36350, 1000.000000000000000 ) ;
#28104=AXIS2_PLACEMENT_3D ( 'NONE', #12412, #87379, #47354 ) ;
#28161=CARTESIAN_POINT ( 'NONE',  ( 47.62500000000000000, 111.1250000000000000, 219.0749999999999886 ) ) ;
#28180=DIRECTION ( 'NONE',  ( -1.000000000000000000, 0.000000000000000000, 1.821231995776179916E-16 ) ) ;
#28186=CARTESIAN_POINT ( 'NONE',  ( 52.38749999999999574, 94.53880000000000905, 229.3937500000000114 ) ) ;
#28200=ORIENTED_EDGE ( 'NONE', *, *, #40796, .T. ) ;
#28229=ORIENTED_EDGE ( 'NONE', *, *, #804, .T. ) ;
#28248=CARTESIAN_POINT ( 'NONE',  ( 57.14999999999999858, 69.84999999999999432, 326.2630000000000337 ) ) ;
#28274=VERTEX_POINT ( 'NONE', #35239 ) ;
#28281=CONICAL_SURFACE ( 'NONE', #79086, 5.562599999999973122, 1.029744258676653645 ) ;
#28284=DIRECTION ( 'NONE',  ( 1.000000000000000000, 0.000000000000000000, 0.000000000000000000 ) ) ;
#28296=DIRECTION ( 'NONE',  ( 0.000000000000000000, 0.000000000000000000, -1.000000000000000000 ) ) ;
#28318=CARTESIAN_POINT ( 'NONE',  ( 7.620115932400938793E-15, 60.82030000000000314, 221.5895999999999901 ) ) ;
#28319=EDGE_CURVE ( 'NONE', #56872, #76329, #84765, .T. ) ;
#28429=ORIENTED_EDGE ( 'NONE', *, *, #9742, .F. ) ;
#28476=AXIS2_PLACEMENT_3D ( 'NONE', #15424, #32044, #25229 ) ;
#28477=DIRECTION ( 'NONE',  ( 0.000000000000000000, 1.000000000000000000, 0.000000000000000000 ) ) ;
#28498=DIRECTION ( 'NONE',  ( -1.000000000000000000, 0.000000000000000000, 0.000000000000000000 ) ) ;
#28503=LINE ( 'NONE', #48045, #19199 ) ;
#28508=CARTESIAN_POINT ( 'NONE',  ( 0.000000000000000000, 95.14999999999999147, 118.5560000000000116 ) ) ;
#28513=FACE_OUTER_BOUND ( 'NONE', #80288, .T. ) ;
#28572=EDGE_LOOP ( 'NONE', ( #59532, #45621 ) ) ;
#28625=AXIS2_PLACEMENT_3D ( 'NONE', #21562, #63332, #2005 ) ;
#28626=AXIS2_PLACEMENT_3D ( 'NONE', #55743, #83489, #21262 ) ;
#28684=DIRECTION ( 'NONE',  ( 5.782411586589351722E-16, 0.000000000000000000, 1.000000000000000000 ) ) ;
#28685=DIRECTION ( 'NONE',  ( -1.784063995862374817E-16, 0.000000000000000000, -1.000000000000000000 ) ) ;
#28716=VECTOR ( 'NONE', #22357, 999.9999999999998863 ) ;
#28740=SHAPE_REPRESENTATION ( 'Hydraulic Index Locking Pin', ( #50656 ), #14432 ) ;
#28761=VERTEX_POINT ( 'NONE', #50995 ) ;
#28774=FACE_BOUND ( 'NONE', #59939, .T. ) ;
#28790=CARTESIAN_POINT ( 'NONE',  ( 34.92499999999999716, 87.13271776169258942, 310.8325000000000387 ) ) ;
#28868=VECTOR ( 'NONE', #80056, 1000.000000000000000 ) ;
#28912=AXIS2_PLACEMENT_3D ( 'NONE', #11769, #52613, #79934 ) ;
#28962=VECTOR ( 'NONE', #10322, 1000.000000000000000 ) ;
#28991=DIRECTION ( 'NONE',  ( 0.000000000000000000, 0.000000000000000000, -1.000000000000000000 ) ) ;
#29000=LINE ( 'NONE', #49415, #58167 ) ;
#29017=EDGE_CURVE ( 'NONE', #14032, #31593, #53993, .T. ) ;
#29059=PLANE ( 'NONE',  #21686 ) ;
#29120=CARTESIAN_POINT ( 'NONE',  ( 57.14999999999999858, 60.86974387893089755, 297.6879999999999882 ) ) ;
#29171=CARTESIAN_POINT ( 'NONE',  ( 50.79999999999999716, 73.02500000000000568, 257.1750000000000114 ) ) ;
#29179=CARTESIAN_POINT ( 'NONE',  ( 0.000000000000000000, 65.60000000000000853, 118.5560000000000116 ) ) ;
#29241=AXIS2_PLACEMENT_3D ( 'NONE', #36223, #1261, #28498 ) ;
#29325=AXIS2_PLACEMENT_3D ( 'NONE', #89413, #59880, #6283 ) ;
#29361=ORIENTED_EDGE ( 'NONE', *, *, #50805, .F. ) ;
#29396=ORIENTED_EDGE ( 'NONE', *, *, #78215, .T. ) ;
#29398=EDGE_CURVE ( 'NONE', #55059, #65439, #11735, .T. ) ;
#29416=DIRECTION ( 'NONE',  ( 1.000000000000000000, 0.000000000000000000, 1.248844797103662002E-15 ) ) ;
#29470=VERTEX_POINT ( 'NONE', #68900 ) ;
#29496=ORIENTED_EDGE ( 'NONE', *, *, #67266, .T. ) ;
#29506=DIRECTION ( 'NONE',  ( 0.000000000000000000, 0.000000000000000000, 1.000000000000000000 ) ) ;
#29528=CARTESIAN_POINT ( 'NONE',  ( 34.92499999999999716, 82.54999999999999716, 315.3410000000000082 ) ) ;
#29583=CARTESIAN_POINT ( 'NONE',  ( 67.65734841870819594, 95.25000000000000000, 346.9005000000000223 ) ) ;
#29592=CARTESIAN_POINT ( 'NONE',  ( 23.07567186625316680, 87.18950910861248360, 301.8082642732044292 ) ) ;
#29593=ADVANCED_FACE ( 'NONE', ( #34834 ), #15307, .F. ) ;
#29614=CARTESIAN_POINT ( 'NONE',  ( 53.97500000000000142, 69.84999999999999432, 283.4005000000000223 ) ) ;
#29701=ADVANCED_FACE ( 'NONE', ( #69815 ), #77525, .T. ) ;
#29705=AXIS2_PLACEMENT_3D ( 'NONE', #37598, #16262, #30337 ) ;
#29717=EDGE_LOOP ( 'NONE', ( #75609, #80454, #28229, #42783 ) ) ;
#29738=ORIENTED_EDGE ( 'NONE', *, *, #42937, .T. ) ;
#29739=ORIENTED_EDGE ( 'NONE', *, *, #53872, .F. ) ;
#29793=CARTESIAN_POINT ( 'NONE',  ( 7.661254700127833495, 82.54999999999999716, 317.6630000000000109 ) ) ;
#29803=EDGE_LOOP ( 'NONE', ( #10540, #30921, #68167, #65329, #15218 ) ) ;
#29838=VECTOR ( 'NONE', #15914, 1000.000000000000227 ) ;
#29865=CYLINDRICAL_SURFACE ( 'NONE', #29241, 16.09746158385918946 ) ;
#29873=ORIENTED_EDGE ( 'NONE', *, *, #27048, .F. ) ;
#29880=CARTESIAN_POINT ( 'NONE',  ( 6.309809686823171226, 93.48723291110538014, 118.3899544324468849 ) ) ;
#29889=DIRECTION ( 'NONE',  ( 0.000000000000000000, 0.000000000000000000, -1.000000000000000000 ) ) ;
#29893=DIRECTION ( 'NONE',  ( -1.000000000000000000, 0.000000000000000000, 0.000000000000000000 ) ) ;
#29904=ORIENTED_EDGE ( 'NONE', *, *, #73779, .F. ) ;
#29927=VECTOR ( 'NONE', #47219, 1000.000000000000000 ) ;
#29971=CARTESIAN_POINT ( 'NONE',  ( 67.65734841870819594, 69.84999999999999432, 346.9005000000000223 ) ) ;
#29981=EDGE_LOOP ( 'NONE', ( #8603, #78001, #83104, #21845, #88843 ) ) ;
#29989=DIRECTION ( 'NONE',  ( -1.986798540846734824E-16, 0.000000000000000000, 1.000000000000000000 ) ) ;
#30008=DIRECTION ( 'NONE',  ( 1.000000000000000000, 0.000000000000000000, 0.000000000000000000 ) ) ;
#30038=VECTOR ( 'NONE', #69853, 1000.000000000000000 ) ;
#30040=EDGE_LOOP ( 'NONE', ( #10806, #26053, #43601, #79388 ) ) ;
#30048=CARTESIAN_POINT ( 'NONE',  ( 23.75644972749645589, 82.86210472292506779, 307.6498562130229857 ) ) ;
#30061=AXIS2_PLACEMENT_3D ( 'NONE', #52884, #25671, #18404 ) ;
#30066=CARTESIAN_POINT ( 'NONE',  ( -7.661254700127833495, 82.54999999999999716, 275.4630000000000223 ) ) ;
#30078=CARTESIAN_POINT ( 'NONE',  ( 57.14999999999999858, 95.25000000000000000, 300.8629999999999995 ) ) ;
#30092=LINE ( 'NONE', #15579, #65863 ) ;
#30093=ORIENTED_EDGE ( 'NONE', *, *, #45260, .F. ) ;
#30122=VECTOR ( 'NONE', #53120, 1000.000000000000000 ) ;
#30140=DIRECTION ( 'NONE',  ( 0.000000000000000000, 0.000000000000000000, -1.000000000000000000 ) ) ;
#30177=CARTESIAN_POINT ( 'NONE',  ( 28.57499999999999929, 87.13271776169270311, 294.9574999999999818 ) ) ;
#30218=EDGE_CURVE ( 'NONE', #24379, #49324, #16972, .T. ) ;
#30267=DIRECTION ( 'NONE',  ( 0.000000000000000000, 1.000000000000000000, 0.000000000000000000 ) ) ;
#30278=CARTESIAN_POINT ( 'NONE',  ( 88.90000000000000568, 66.67499999999999716, 342.8999999999999773 ) ) ;
#30308=CARTESIAN_POINT ( 'NONE',  ( 82.54999999999999716, 95.25000000000000000, 358.0130000000000337 ) ) ;
#30337=DIRECTION ( 'NONE',  ( 1.000000000000000000, 0.000000000000000000, 0.000000000000000000 ) ) ;
#30353=ORIENTED_EDGE ( 'NONE', *, *, #36171, .F. ) ;
#30407=ORIENTED_EDGE ( 'NONE', *, *, #45198, .T. ) ;
#30522=DIRECTION ( 'NONE',  ( 0.000000000000000000, 0.000000000000000000, 1.000000000000000000 ) ) ;
#30528=ORIENTED_EDGE ( 'NONE', *, *, #75951, .T. ) ;
#30541=AXIS2_PLACEMENT_3D ( 'NONE', #21419, #70013, #1426 ) ;
#30571=ADVANCED_FACE ( 'NONE', ( #78984 ), #17642, .F. ) ;
#30606=VECTOR ( 'NONE', #647, 1000.000000000000000 ) ;
#30728=ADVANCED_FACE ( 'NONE', ( #25334 ), #6689, .T. ) ;
#30754=DIRECTION ( 'NONE',  ( -0.8571673007021118895, 1.049727191138617833E-16, 0.5150380749100549327 ) ) ;
#30759=FACE_OUTER_BOUND ( 'NONE', #64764, .T. ) ;
#30787=ORIENTED_EDGE ( 'NONE', *, *, #45147, .F. ) ;
#30814=LINE ( 'NONE', #59839, #88313 ) ;
#30835=EDGE_LOOP ( 'NONE', ( #42380, #9168, #38271, #77503 ) ) ;
#30868=VERTEX_POINT ( 'NONE', #55702 ) ;
#30921=ORIENTED_EDGE ( 'NONE', *, *, #37751, .T. ) ;
#31013=EDGE_CURVE ( 'NONE', #28274, #89072, #2582, .T. ) ;
#31038=ADVANCED_FACE ( 'NONE', ( #24796 ), #23480, .F. ) ;
#31066=ORIENTED_EDGE ( 'NONE', *, *, #14200, .F. ) ;
#31067=ORIENTED_EDGE ( 'NONE', *, *, #88184, .T. ) ;
#31097=DIRECTION ( 'NONE',  ( 0.000000000000000000, -1.000000000000000000, 0.000000000000000000 ) ) ;
#31115=AXIS2_PLACEMENT_3D ( 'NONE', #49535, #16388, #64974 ) ;
#31116=PLANE ( 'NONE',  #703 ) ;
#31158=VERTEX_POINT ( 'NONE', #81127 ) ;
#31160=DIRECTION ( 'NONE',  ( -1.000000000000000000, -1.561055996379579722E-16, 0.000000000000000000 ) ) ;
#31192=VECTOR ( 'NONE', #3886, 1000.000000000000000 ) ;
#31282=EDGE_LOOP ( 'NONE', ( #30528, #33211, #81327, #38182 ) ) ;
#31324=DIRECTION ( 'NONE',  ( -1.000000000000000000, 0.000000000000000000, 0.000000000000000000 ) ) ;
#31330=AXIS2_PLACEMENT_3D ( 'NONE', #35828, #8138, #6785 ) ;
#31345=DIRECTION ( 'NONE',  ( 0.000000000000000000, -1.000000000000000000, 0.000000000000000000 ) ) ;
#31365=ORIENTED_EDGE ( 'NONE', *, *, #46869, .T. ) ;
#31368=CARTESIAN_POINT ( 'NONE',  ( 23.04771283656240399, 87.28173361942839392, 302.2699916481048490 ) ) ;
#31379=CARTESIAN_POINT ( 'NONE',  ( 0.000000000000000000, 95.14999999999999147, 118.5560000000000116 ) ) ;
#31420=CARTESIAN_POINT ( 'NONE',  ( 74.98969683741650272, 82.54999999999999716, 346.9005000000000223 ) ) ;
#31543=FACE_OUTER_BOUND ( 'NONE', #37021, .T. ) ;
#31578=VERTEX_POINT ( 'NONE', #81466 ) ;
#31593=VERTEX_POINT ( 'NONE', #67346 ) ;
#31638=ORIENTED_EDGE ( 'NONE', *, *, #8057, .F. ) ;
#31649=CARTESIAN_POINT ( 'NONE',  ( 52.99265158129180264, 69.84999999999999432, 346.9005000000000223 ) ) ;
#31677=AXIS2_PLACEMENT_3D ( 'NONE', #45462, #86832, #80929 ) ;
#31728=DIRECTION ( 'NONE',  ( -1.000000000000000000, 0.000000000000000000, 0.000000000000000000 ) ) ;
#31765=FACE_OUTER_BOUND ( 'NONE', #25197, .T. ) ;
#31771=DIRECTION ( 'NONE',  ( 0.000000000000000000, 0.000000000000000000, -1.000000000000000000 ) ) ;
#31809=VERTEX_POINT ( 'NONE', #83245 ) ;
#31820=ORIENTED_EDGE ( 'NONE', *, *, #49475, .T. ) ;
#31861=CARTESIAN_POINT ( 'NONE',  ( -44.45000000000000284, 114.2999999999999972, 257.1750000000000114 ) ) ;
#31882=FACE_OUTER_BOUND ( 'NONE', #10299, .T. ) ;
#31957=ORIENTED_EDGE ( 'NONE', *, *, #29017, .T. ) ;
#31975=EDGE_CURVE ( 'NONE', #50744, #31593, #40400, .T. ) ;
#32004=CIRCLE ( 'NONE', #59545, 12.44600000000001216 ) ;
#32027=CARTESIAN_POINT ( 'NONE',  ( 34.92499999999999716, 66.67499999999999716, 346.0750000000000455 ) ) ;
#32044=DIRECTION ( 'NONE',  ( 0.000000000000000000, -1.000000000000000000, 0.000000000000000000 ) ) ;
#32111=DIRECTION ( 'NONE',  ( 0.000000000000000000, -1.000000000000000000, 0.000000000000000000 ) ) ;
#32121=DIRECTION ( 'NONE',  ( 1.000000000000000000, 0.000000000000000000, 0.000000000000000000 ) ) ;
#32213=ORIENTED_EDGE ( 'NONE', *, *, #59812, .F. ) ;
#32252=EDGE_LOOP ( 'NONE', ( #22354, #10779, #78069, #31638, #44895 ) ) ;
#32319=FILL_AREA_STYLE ('',( #74122 ) ) ;
#32334=CARTESIAN_POINT ( 'NONE',  ( 6.812220284937080487E-16, 50.79999999999999716, 271.1195999999999913 ) ) ;
#32344=DIRECTION ( 'NONE',  ( 0.000000000000000000, 0.000000000000000000, 1.000000000000000000 ) ) ;
#32424=FACE_OUTER_BOUND ( 'NONE', #10936, .T. ) ;
#32426=CARTESIAN_POINT ( 'NONE',  ( 28.57499999999999929, 73.38456447661469895, 302.8950000000000387 ) ) ;
#32484=CARTESIAN_POINT ( 'NONE',  ( 74.98969683741650272, 82.54999999999999716, 346.9005000000000223 ) ) ;
#32493=EDGE_LOOP ( 'NONE', ( #70239, #60907, #62862, #79249 ) ) ;
#32533=ADVANCED_FACE ( 'NONE', ( #79795 ), #29059, .T. ) ;
#32538=LINE ( 'NONE', #60243, #85946 ) ;
#32579=VERTEX_POINT ( 'NONE', #3472 ) ;
#32657=LINE ( 'NONE', #68083, #39602 ) ;
#32659=FACE_OUTER_BOUND ( 'NONE', #56422, .T. ) ;
#32709=DIRECTION ( 'NONE',  ( 1.000000000000000000, 0.000000000000000000, 0.000000000000000000 ) ) ;
#32719=ORIENTED_EDGE ( 'NONE', *, *, #33393, .F. ) ;
#32725=CARTESIAN_POINT ( 'NONE',  ( 23.22105850524281934, 78.42056979272489059, 305.2876152861762193 ) ) ;
#32748=FACE_OUTER_BOUND ( 'NONE', #82031, .T. ) ;
#32773=FACE_OUTER_BOUND ( 'NONE', #74059, .T. ) ;
#32777=ORIENTED_EDGE ( 'NONE', *, *, #49709, .T. ) ;
#32822=PLANE ( 'NONE',  #20005 ) ;
#32844=CARTESIAN_POINT ( 'NONE',  ( -10.70530292206537482, 89.20793846563920226, 118.0719063050892998 ) ) ;
#32852=PLANE ( 'NONE',  #20470 ) ;
#32857=ORIENTED_EDGE ( 'NONE', *, *, #61807, .F. ) ;
#32950=VERTEX_POINT ( 'NONE', #86936 ) ;
#32977=ORIENTED_EDGE ( 'NONE', *, *, #43324, .T. ) ;
#33003=EDGE_LOOP ( 'NONE', ( #72303, #18661, #4641, #55285 ) ) ;
#33021=ORIENTED_EDGE ( 'NONE', *, *, #22868, .T. ) ;
#33054=ORIENTED_EDGE ( 'NONE', *, *, #70835, .T. ) ;
#33113=DIRECTION ( 'NONE',  ( 0.000000000000000000, -1.000000000000000000, 0.000000000000000000 ) ) ;
#33115=ORIENTED_EDGE ( 'NONE', *, *, #88125, .T. ) ;
#33159=EDGE_CURVE ( 'NONE', #53213, #75348, #36198, .T. ) ;
#33179=CARTESIAN_POINT ( 'NONE',  ( 23.68742839265041766, 81.00938505711215498, 307.4121377794205614 ) ) ;
#33187=ORIENTED_EDGE ( 'NONE', *, *, #77502, .T. ) ;
#33201=ORIENTED_EDGE ( 'NONE', *, *, #24700, .F. ) ;
#33211=ORIENTED_EDGE ( 'NONE', *, *, #11762, .F. ) ;
#33228=CARTESIAN_POINT ( 'NONE',  ( -7.685739755354498826, 72.53188479423953083, 118.3085854593769568 ) ) ;
#33277=DIRECTION ( 'NONE',  ( -1.000000000000000000, 0.000000000000000000, 9.299908063537909262E-17 ) ) ;
#33299=AXIS2_PLACEMENT_3D ( 'NONE', #58019, #51189, #64397 ) ;
#33312=LINE ( 'NONE', #83264, #952 ) ;
#33342=CIRCLE ( 'NONE', #53665, 6.557978799109520196 ) ;
#33361=ORIENTED_EDGE ( 'NONE', *, *, #77085, .T. ) ;
#33370=DIRECTION ( 'NONE',  ( -1.000000000000000000, 0.000000000000000000, 0.000000000000000000 ) ) ;
#33390=EDGE_LOOP ( 'NONE', ( #85836, #82180, #21244, #25535, #11532, #48333 ) ) ;
#33393=EDGE_CURVE ( 'NONE', #44353, #70068, #83699, .T. ) ;
#33451=FACE_OUTER_BOUND ( 'NONE', #6698, .T. ) ;
#33491=CARTESIAN_POINT ( 'NONE',  ( 31.75000000000000000, 66.67499999999999716, 346.0750000000000455 ) ) ;
#33501=AXIS2_PLACEMENT_3D ( 'NONE', #79129, #44122, #2821 ) ;
#33535=CIRCLE ( 'NONE', #64025, 12.44600000000001216 ) ;
#33601=CONICAL_SURFACE ( 'NONE', #45194, 6.857999999999975671, 0.02993239667170383839 ) ;
#33680=( NAMED_UNIT ( * ) PLANE_ANGLE_UNIT ( ) SI_UNIT ( $, .RADIAN. ) );
#33719=ADVANCED_FACE ( 'NONE', ( #82712 ), #75436, .T. ) ;
#33739=EDGE_CURVE ( 'NONE', #40033, #34033, #76771, .T. ) ;
#33745=AXIS2_PLACEMENT_3D ( 'NONE', #82658, #20415, #75818 ) ;
#33770=EDGE_LOOP ( 'NONE', ( #64522, #48801, #25662, #1350 ) ) ;
#33790=CARTESIAN_POINT ( 'NONE',  ( 47.62500000000000000, 69.84999999999999432, 283.4005000000000223 ) ) ;
#33802=CARTESIAN_POINT ( 'NONE',  ( -7.661254700127833495, 82.54999999999999716, 320.6630000000000109 ) ) ;
#33891=CARTESIAN_POINT ( 'NONE',  ( 0.000000000000000000, 60.82030000000000314, 259.9944000000000415 ) ) ;
#33894=ADVANCED_FACE ( 'NONE', ( #75877, #56303 ), #83157, .T. ) ;
#33907=CARTESIAN_POINT ( 'NONE',  ( 47.62500000000000000, 94.53880000000000905, 254.7937499999999886 ) ) ;
#33927=VECTOR ( 'NONE', #75850, 1000.000000000000000 ) ;
#33958=ORIENTED_EDGE ( 'NONE', *, *, #50558, .F. ) ;
#33992=ORIENTED_EDGE ( 'NONE', *, *, #70618, .T. ) ;
#34010=ORIENTED_EDGE ( 'NONE', *, *, #25100, .F. ) ;
#34018=CARTESIAN_POINT ( 'NONE',  ( 45.66030316258350297, 82.54999999999999716, 346.9005000000000223 ) ) ;
#34033=VERTEX_POINT ( 'NONE', #29971 ) ;
#34047=AXIS2_PLACEMENT_3D ( 'NONE', #25001, #39065, #66772 ) ;
#34055=CARTESIAN_POINT ( 'NONE',  ( 23.08506796337472622, 77.94149302405480739, 304.1359325411505097 ) ) ;
#34142=CARTESIAN_POINT ( 'NONE',  ( 47.62500000000000000, 94.53880000000000905, 250.8250000000000171 ) ) ;
#34181=CARTESIAN_POINT ( 'NONE',  ( -11.65927676768451171, 87.37969543255378824, 117.9816103563385781 ) ) ;
#34238=EDGE_CURVE ( 'NONE', #89758, #12738, #25331, .T. ) ;
#34257=CARTESIAN_POINT ( 'NONE',  ( 67.65734841870819594, 69.84999999999999432, 346.9005000000000223 ) ) ;
#34275=CARTESIAN_POINT ( 'NONE',  ( 38.10000000000000142, 95.25000000000000000, 358.0130000000000337 ) ) ;
#34321=EDGE_CURVE ( 'NONE', #68627, #31158, #19873, .T. ) ;
#34339=LINE ( 'NONE', #62045, #26835 ) ;
#34348=DIRECTION ( 'NONE',  ( 0.000000000000000000, -1.000000000000000000, 0.000000000000000000 ) ) ;
#34352=CARTESIAN_POINT ( 'NONE',  ( 31.75000000000000000, 66.67499999999999716, 292.1000000000000227 ) ) ;
#34385=ORIENTED_EDGE ( 'NONE', *, *, #24700, .T. ) ;
#34393=CARTESIAN_POINT ( 'NONE',  ( 57.14999999999999858, 60.86974387893089755, 300.8629999999999995 ) ) ;
#34441=DIRECTION ( 'NONE',  ( 1.092739197465703932E-16, -1.000000000000000000, 0.000000000000000000 ) ) ;
#34445=LINE ( 'NONE', #57118, #25086 ) ;
#34450=LINE ( 'NONE', #69434, #76675 ) ;
#34527=B_SPLINE_CURVE_WITH_KNOTS ( 'NONE', 3,
 ( #44596, #65508, #24620, #52286, #38682, #66387, #27302, #80950, #60465, #53179, #26851, #33228, #18698, #47733, #88209, #25968, #60926, #81842, #53633, #54086, #19591, #82746, #89545, #12796, #88654, #81406 ),
 .UNSPECIFIED., .F., .F.,
 ( 4, 2, 2, 2, 2, 2, 2, 2, 2, 2, 2, 2, 4 ),
 ( 0.01971515547648590785, 0.02094678046519103318, 0.02217840545389616197, 0.02464165543130641262, 0.02587328042001153100, 0.02710490540871664938, 0.02956815538612688615, 0.03203140536353712292, 0.03326303035224223437, 0.03449465534094735275, 0.03695790531835754789, 0.03818953030706266627, 0.03942115529576777772 ),
 .UNSPECIFIED. ) ;
#34530=AXIS2_PLACEMENT_3D ( 'NONE', #6840, #81817, #7739 ) ;
#34539=ORIENTED_EDGE ( 'NONE', *, *, #36885, .T. ) ;
#34553=FACE_OUTER_BOUND ( 'NONE', #87819, .T. ) ;
#34574=VERTEX_POINT ( 'NONE', #12850 ) ;
#34579=DIRECTION ( 'NONE',  ( -0.4999999999999998890, -0.8660254037844387076, 0.000000000000000000 ) ) ;
#34596=CARTESIAN_POINT ( 'NONE',  ( 7.661254700127842376, 69.45253841614081125, 317.6630000000000109 ) ) ;
#34597=LINE ( 'NONE', #39614, #51553 ) ;
#34608=LINE ( 'NONE', #55475, #80631 ) ;
#34702=EDGE_LOOP ( 'NONE', ( #72042, #29361 ) ) ;
#34749=EDGE_CURVE ( 'NONE', #75698, #8926, #38594, .T. ) ;
#34752=ORIENTED_EDGE ( 'NONE', *, *, #59207, .F. ) ;
#34761=VERTEX_POINT ( 'NONE', #69595 ) ;
#34834=FACE_OUTER_BOUND ( 'NONE', #64642, .T. ) ;
#34835=ADVANCED_FACE ( 'NONE', ( #22346 ), #63306, .F. ) ;
#34882=CARTESIAN_POINT ( 'NONE',  ( 12.51828547952651682, 84.20585872486917367, 117.8933604834281539 ) ) ;
#34906=DIRECTION ( 'NONE',  ( 1.000000000000000000, 0.000000000000000000, 0.000000000000000000 ) ) ;
#34919=LINE ( 'NONE', #14497, #36796 ) ;
#34950=LINE ( 'NONE', #69487, #33927 ) ;
#35024=CARTESIAN_POINT ( 'NONE',  ( 60.32499999999999574, 82.54999999999999716, 358.0130000000000337 ) ) ;
#35070=DIRECTION ( 'NONE',  ( 1.748382715945130353E-14, 0.000000000000000000, -1.000000000000000000 ) ) ;
#35083=CIRCLE ( 'NONE', #38016, 16.09746158385918946 ) ;
#35188=LINE ( 'NONE', #18544, #43957 ) ;
#35230=DIRECTION ( 'NONE',  ( -1.000000000000000000, 0.000000000000000000, 0.000000000000000000 ) ) ;
#35239=CARTESIAN_POINT ( 'NONE',  ( 88.90000000000000568, 69.84999999999999432, 342.8999999999999773 ) ) ;
#35274=DIRECTION ( 'NONE',  ( 1.000000000000000000, 0.000000000000000000, 0.000000000000000000 ) ) ;
#35322=APPLICATION_CONTEXT ( 'automotive_design' ) ;
#35369=ORIENTED_EDGE ( 'NONE', *, *, #40169, .T. ) ;
#35398=CARTESIAN_POINT ( 'NONE',  ( 6.938893903907229955E-15, 50.79999999999999716, 209.1689999999999827 ) ) ;
#35448=VERTEX_POINT ( 'NONE', #24909 ) ;
#35455=FACE_OUTER_BOUND ( 'NONE', #84833, .T. ) ;
#35458=AXIS2_PLACEMENT_3D ( 'NONE', #15373, #58030, #78503 ) ;
#35464=LINE ( 'NONE', #29120, #75034 ) ;
#35472=AXIS2_PLACEMENT_3D ( 'NONE', #8934, #8018, #9360 ) ;
#35486=CARTESIAN_POINT ( 'NONE',  ( 82.54999999999999716, 69.84999999999999432, 280.2255000000000109 ) ) ;
#35507=CARTESIAN_POINT ( 'NONE',  ( 52.38749999999999574, 94.53880000000000905, 250.8250000000000171 ) ) ;
#35609=EDGE_CURVE ( 'NONE', #86449, #65439, #35741, .T. ) ;
#35615=LINE ( 'NONE', #77408, #30606 ) ;
#35622=ORIENTED_EDGE ( 'NONE', *, *, #27074, .T. ) ;
#35627=CARTESIAN_POINT ( 'NONE',  ( -12.59999999999999964, 82.54999999999999716, 117.8845415480757595 ) ) ;
#35638=ORIENTED_EDGE ( 'NONE', *, *, #88125, .F. ) ;
#35680=DIRECTION ( 'NONE',  ( 1.000000000000000000, 0.000000000000000000, -0.000000000000000000 ) ) ;
#35726=FACE_OUTER_BOUND ( 'NONE', #64253, .T. ) ;
#35741=LINE ( 'NONE', #13964, #89508 ) ;
#35775=CARTESIAN_POINT ( 'NONE',  ( 10.00863283467136711, 90.24885462885215759, 118.1336793349710632 ) ) ;
#35801=VECTOR ( 'NONE', #86093, 1000.000000000000114 ) ;
#35828=CARTESIAN_POINT ( 'NONE',  ( 34.92499999999999716, 82.54999999999999716, 302.8950000000000387 ) ) ;
#35841=CARTESIAN_POINT ( 'NONE',  ( 7.661254700127844153, 66.45253841614081125, 317.6630000000000109 ) ) ;
#35852=ADVANCED_FACE ( 'NONE', ( #60642 ), #74739, .F. ) ;
#35855=CARTESIAN_POINT ( 'NONE',  ( -23.75871628398702384, 82.54999999999999716, 317.6630000000000109 ) ) ;
#35868=AXIS2_PLACEMENT_3D ( 'NONE', #54928, #14073, #20452 ) ;
#35876=CARTESIAN_POINT ( 'NONE',  ( 52.38749999999999574, 94.53880000000000905, 225.4249999999999829 ) ) ;
#35882=EDGE_LOOP ( 'NONE', ( #8352, #52732, #82166, #46597 ) ) ;
#35883=AXIS2_PLACEMENT_3D ( 'NONE', #54406, #53960, #62592 ) ;
#35892=DIRECTION ( 'NONE',  ( 1.000000000000000000, 0.000000000000000000, 0.000000000000000000 ) ) ;
#35927=CARTESIAN_POINT ( 'NONE',  ( 38.10000000000000142, 95.25000000000000000, 283.4005000000000223 ) ) ;
#35950=AXIS2_PLACEMENT_3D ( 'NONE', #88418, #47041, #41134 ) ;
#35955=AXIS2_PLACEMENT_3D ( 'NONE', #34596, #55913, #28684 ) ;
#36071=CARTESIAN_POINT ( 'NONE',  ( 6.938893903907229955E-15, 60.82030000000000314, 210.4643999999999835 ) ) ;
#36078=LINE ( 'NONE', #34275, #9612 ) ;
#36096=PLANE ( 'NONE',  #72326 ) ;
#36171=EDGE_CURVE ( 'NONE', #82352, #58613, #61100, .T. ) ;
#36198=CIRCLE ( 'NONE', #81214, 3.174999999999997158 ) ;
#36223=CARTESIAN_POINT ( 'NONE',  ( 7.661254700127833495, 82.54999999999999716, 320.6630000000000109 ) ) ;
#36253=CIRCLE ( 'NONE', #14475, 13.09746158385919124 ) ;
#36350=DIRECTION ( 'NONE',  ( -1.000000000000000000, 0.000000000000000000, -9.713237310806269221E-16 ) ) ;
#36351=PLANE ( 'NONE',  #13868 ) ;
#36364=VECTOR ( 'NONE', #58378, 1000.000000000000000 ) ;
#36403=DIRECTION ( 'NONE',  ( 0.000000000000000000, -1.000000000000000000, 0.000000000000000000 ) ) ;
#36407=CARTESIAN_POINT ( 'NONE',  ( 47.62500000000000000, 94.53880000000000905, 246.8562499999999886 ) ) ;
#36466=EDGE_CURVE ( 'NONE', #7668, #80899, #453, .T. ) ;
#36482=CARTESIAN_POINT ( 'NONE',  ( 31.75000000000000000, 69.84999999999999432, 292.1000000000000227 ) ) ;
#36601=CARTESIAN_POINT ( 'NONE',  ( -7.661254700127832606, 95.64746158385918307, 317.6630000000000109 ) ) ;
#36625=ORIENTED_EDGE ( 'NONE', *, *, #19744, .T. ) ;
#36628=VECTOR ( 'NONE', #51223, 999.9999999999998863 ) ;
#36693=CARTESIAN_POINT ( 'NONE',  ( 8.311119758860220585, 92.02930930504943774, 118.2647611583656300 ) ) ;
#36707=DIRECTION ( 'NONE',  ( 0.000000000000000000, 0.000000000000000000, -1.000000000000000000 ) ) ;
#36729=CARTESIAN_POINT ( 'NONE',  ( -7.661254700127832606, 98.64746158385918307, 275.4630000000000223 ) ) ;
#36735=ORIENTED_EDGE ( 'NONE', *, *, #39026, .F. ) ;
#36746=CARTESIAN_POINT ( 'NONE',  ( 7.661254700127833495, 82.54999999999999716, 317.6630000000000109 ) ) ;
#36796=VECTOR ( 'NONE', #69453, 999.9999999999998863 ) ;
#36885=EDGE_CURVE ( 'NONE', #16110, #53327, #25815, .T. ) ;
#36920=CARTESIAN_POINT ( 'NONE',  ( 69.25310000000000343, 82.54999999999999716, 344.4418053999999643 ) ) ;
#36923=CARTESIAN_POINT ( 'NONE',  ( -44.45000000000000284, 50.79999999999999716, 275.4630000000000223 ) ) ;
#36947=CARTESIAN_POINT ( 'NONE',  ( 34.92499999999999716, 91.71543552338529537, 302.8950000000000387 ) ) ;
#36967=CARTESIAN_POINT ( 'NONE',  ( 10.93445099564298317, 76.23525864503069727, 118.0515728341300559 ) ) ;
#37021=EDGE_LOOP ( 'NONE', ( #79599, #874, #19349, #16244 ) ) ;
#37029=CARTESIAN_POINT ( 'NONE',  ( 0.000000000000000000, 82.54999999999999716, -190.5010000000000048 ) ) ;
#37048=CARTESIAN_POINT ( 'NONE',  ( 44.45000000000000284, 69.84999999999999432, 219.0749999999999886 ) ) ;
#37074=VERTEX_POINT ( 'NONE', #78905 ) ;
#37109=CARTESIAN_POINT ( 'NONE',  ( 28.57499999999999929, 91.71543552338529537, 302.8950000000000387 ) ) ;
#37112=ORIENTED_EDGE ( 'NONE', *, *, #13699, .F. ) ;
#37161=ORIENTED_EDGE ( 'NONE', *, *, #28319, .T. ) ;
#37169=LINE ( 'NONE', #3099, #55619 ) ;
#37287=VERTEX_POINT ( 'NONE', #71537 ) ;
#37329=ORIENTED_EDGE ( 'NONE', *, *, #44569, .T. ) ;
#37360=ORIENTED_EDGE ( 'NONE', *, *, #10249, .F. ) ;
#37367=CARTESIAN_POINT ( 'NONE',  ( 7.620115932400929327E-15, 67.86880000000000734, 221.5895999999999901 ) ) ;
#37394=ORIENTED_EDGE ( 'NONE', *, *, #66024, .F. ) ;
#37418=CARTESIAN_POINT ( 'NONE',  ( 1.640888995811506934, 70.02979118506246436, 118.5474374850178094 ) ) ;
#37504=CARTESIAN_POINT ( 'NONE',  ( 7.661254700127833495, 82.54999999999999716, 320.6630000000000109 ) ) ;
#37540=DIRECTION ( 'NONE',  ( 0.000000000000000000, -1.000000000000000000, 0.000000000000000000 ) ) ;
#37588=ADVANCED_FACE ( 'NONE', ( #26342 ), #79399, .F. ) ;
#37592=PLANE ( 'NONE',  #4497 ) ;
#37594=ORIENTED_EDGE ( 'NONE', *, *, #54344, .F. ) ;
#37598=CARTESIAN_POINT ( 'NONE',  ( 60.32499999999999574, 82.54999999999999716, 335.3740053999999304 ) ) ;
#37624=CARTESIAN_POINT ( 'NONE',  ( 53.97500000000000142, 95.25000000000000000, 283.4005000000000223 ) ) ;
#37629=ORIENTED_EDGE ( 'NONE', *, *, #7761, .T. ) ;
#37630=AXIS2_PLACEMENT_3D ( 'NONE', #81324, #61287, #88127 ) ;
#37733=CARTESIAN_POINT ( 'NONE',  ( 31.75000000000000000, 69.84999999999999432, 346.0750000000000455 ) ) ;
#37745=DIRECTION ( 'NONE',  ( 0.000000000000000000, -1.000000000000000000, 0.000000000000000000 ) ) ;
#37751=EDGE_CURVE ( 'NONE', #27014, #11575, #83722, .T. ) ;
#37756=CARTESIAN_POINT ( 'NONE',  ( 23.12955879343030574, 87.00686711072398793, 301.2092494891036267 ) ) ;
#37808=ORIENTED_EDGE ( 'NONE', *, *, #64836, .F. ) ;
#37830=CARTESIAN_POINT ( 'NONE',  ( 50.06333974046790303, 82.54999999999999716, 344.4418053999999643 ) ) ;
#37843=ORIENTED_EDGE ( 'NONE', *, *, #72446, .F. ) ;
#37899=ORIENTED_EDGE ( 'NONE', *, *, #23966, .F. ) ;
#37961=CARTESIAN_POINT ( 'NONE',  ( 6.349999999999999645, 82.54999999999999716, 302.8950000000000387 ) ) ;
#37987=EDGE_CURVE ( 'NONE', #40995, #54369, #63475, .T. ) ;
#37999=ORIENTED_EDGE ( 'NONE', *, *, #65936, .F. ) ;
#38001=EDGE_CURVE ( 'NONE', #69623, #74022, #76667, .T. ) ;
#38016=AXIS2_PLACEMENT_3D ( 'NONE', #42998, #17111, #65687 ) ;
#38017=ORIENTED_EDGE ( 'NONE', *, *, #72583, .T. ) ;
#38021=CARTESIAN_POINT ( 'NONE',  ( 28.57499999999999929, 87.13271776169270311, 294.9574999999999818 ) ) ;
#38076=DIRECTION ( 'NONE',  ( 1.000000000000000000, -8.621103231412346209E-16, 0.000000000000000000 ) ) ;
#38089=EDGE_CURVE ( 'NONE', #1768, #29470, #11185, .T. ) ;
#38141=CARTESIAN_POINT ( 'NONE',  ( 6.938893903907229955E-15, 50.79999999999999716, 209.1689999999999827 ) ) ;
#38160=ORIENTED_EDGE ( 'NONE', *, *, #40796, .F. ) ;
#38182=ORIENTED_EDGE ( 'NONE', *, *, #15955, .T. ) ;
#38252=( NAMED_UNIT ( * ) PLANE_ANGLE_UNIT ( ) SI_UNIT ( $, .RADIAN. ) );
#38254=LINE ( 'NONE', #3739, #28868 ) ;
#38271=ORIENTED_EDGE ( 'NONE', *, *, #4477, .F. ) ;
#38300=CARTESIAN_POINT ( 'NONE',  ( 6.657252557472873811, 71.84426888462246552, 118.3694437465256328 ) ) ;
#38325=DIRECTION ( 'NONE',  ( -1.000000000000000000, 0.000000000000000000, 9.299908063537896936E-17 ) ) ;
#38333=CARTESIAN_POINT ( 'NONE',  ( 0.000000000000000000, 82.54999999999999716, -190.5010000000000048 ) ) ;
#38359=CARTESIAN_POINT ( 'NONE',  ( 50.79999999999999716, 69.84999999999999432, 219.0749999999999886 ) ) ;
#38388=LINE ( 'NONE', #3437, #67934 ) ;
#38413=DIRECTION ( 'NONE',  ( -0.000000000000000000, 1.000000000000000000, -0.000000000000000000 ) ) ;
#38422=ORIENTED_EDGE ( 'NONE', *, *, #7573, .T. ) ;
#38450=CIRCLE ( 'NONE', #84917, 4.762500000000002842 ) ;
#38456=ADVANCED_FACE ( 'NONE', ( #40019 ), #73646, .F. ) ;
#38491=ADVANCED_FACE ( 'NONE', ( #81827 ), #60915, .F. ) ;
#38520=CARTESIAN_POINT ( 'NONE',  ( 23.75871628398702384, 82.54999999999999716, 317.6630000000000109 ) ) ;
#38577=FACE_BOUND ( 'NONE', #40905, .T. ) ;
#38591=AXIS2_PLACEMENT_3D ( 'NONE', #25009, #52672, #32709 ) ;
#38594=CIRCLE ( 'NONE', #67579, 13.09746158385919124 ) ;
#38656=ORIENTED_EDGE ( 'NONE', *, *, #85183, .T. ) ;
#38682=CARTESIAN_POINT ( 'NONE',  ( -2.061562449364020999, 70.11297175739061061, 118.5387631950859344 ) ) ;
#38691=LINE ( 'NONE', #37367, #44795 ) ;
#38754=ORIENTED_EDGE ( 'NONE', *, *, #2732, .T. ) ;
#38758=ORIENTED_EDGE ( 'NONE', *, *, #13176, .T. ) ;
#38791=VECTOR ( 'NONE', #47601, 1000.000000000000000 ) ;
#38811=DIRECTION ( 'NONE',  ( -0.4999999999999998890, 0.8660254037844387076, 0.000000000000000000 ) ) ;
#38842=ORIENTED_EDGE ( 'NONE', *, *, #5310, .T. ) ;
#38894=ORIENTED_EDGE ( 'NONE', *, *, #70304, .F. ) ;
#38932=ORIENTED_EDGE ( 'NONE', *, *, #29398, .F. ) ;
#39002=VERTEX_POINT ( 'NONE', #12668 ) ;
#39003=CARTESIAN_POINT ( 'NONE',  ( 44.45000000000000284, 114.2999999999999972, 206.3750000000000000 ) ) ;
#39026=EDGE_CURVE ( 'NONE', #75933, #76329, #69421, .T. ) ;
#39044=VECTOR ( 'NONE', #78137, 1000.000000000000000 ) ;
#39065=DIRECTION ( 'NONE',  ( 9.299908063537909262E-17, 0.000000000000000000, 1.000000000000000000 ) ) ;
#39087=CARTESIAN_POINT ( 'NONE',  ( 23.11247487853312066, 78.03298490982817270, 301.3540638256986313 ) ) ;
#39088=DIRECTION ( 'NONE',  ( 0.000000000000000000, -1.000000000000000000, 0.000000000000000000 ) ) ;
#39146=CYLINDRICAL_SURFACE ( 'NONE', #73847, 3.174999999999983391 ) ;
#39154=ADVANCED_FACE ( 'NONE', ( #28513 ), #9308, .F. ) ;
#39168=ORIENTED_EDGE ( 'NONE', *, *, #27048, .T. ) ;
#39213=ADVANCED_FACE ( 'NONE', ( #2176 ), #10777, .F. ) ;
#39225=CIRCLE ( 'NONE', #4430, 10.66800000000000459 ) ;
#39262=CARTESIAN_POINT ( 'NONE',  ( 88.90000000000000568, 69.84999999999999432, 244.4749999999999943 ) ) ;
#39318=ORIENTED_EDGE ( 'NONE', *, *, #17993, .T. ) ;
#39360=CARTESIAN_POINT ( 'NONE',  ( 88.90000000000000568, 66.67499999999999716, 244.4749999999999943 ) ) ;
#39380=DIRECTION ( 'NONE',  ( 0.7071067811865531239, 0.000000000000000000, 0.7071067811865420216 ) ) ;
#39409=LINE ( 'NONE', #33491, #60792 ) ;
#39427=EDGE_CURVE ( 'NONE', #24990, #17829, #3948, .T. ) ;
#39477=CARTESIAN_POINT ( 'NONE',  ( 38.10000000000000142, 95.25000000000000000, 358.0130000000000337 ) ) ;
#39518=CARTESIAN_POINT ( 'NONE',  ( 0.000000000000000000, 67.86880000000000734, 265.5569999999999595 ) ) ;
#39562=ORIENTED_EDGE ( 'NONE', *, *, #84842, .T. ) ;
#39602=VECTOR ( 'NONE', #5871, 1000.000000000000000 ) ;
#39614=CARTESIAN_POINT ( 'NONE',  ( 38.10000000000000142, 69.84999999999999432, 358.0130000000000337 ) ) ;
#39643=DIRECTION ( 'NONE',  ( -9.299908063537919123E-17, 0.000000000000000000, -1.000000000000000000 ) ) ;
#39654=CARTESIAN_POINT ( 'NONE',  ( -2.860914336036568528, 94.82778141605180622, 118.5221612204686608 ) ) ;
#39669=DIRECTION ( 'NONE',  ( 1.000000000000000000, 0.000000000000000000, 0.000000000000000000 ) ) ;
#39682=ORIENTED_EDGE ( 'NONE', *, *, #58592, .T. ) ;
#39732=ADVANCED_FACE ( 'NONE', ( #14359 ), #69764, .T. ) ;
#39734=CARTESIAN_POINT ( 'NONE',  ( 44.45000000000000284, 66.67499999999999716, 292.1000000000000227 ) ) ;
#39790=AXIS2_PLACEMENT_3D ( 'NONE', #8099, #36707, #29893 ) ;
#39811=CARTESIAN_POINT ( 'NONE',  ( 38.10000000000000142, 69.84999999999999432, 358.0130000000000337 ) ) ;
#39826=ORIENTED_EDGE ( 'NONE', *, *, #75022, .F. ) ;
#39834=CARTESIAN_POINT ( 'NONE',  ( 49.65699999999999648, 82.54999999999999716, 358.0130000000000337 ) ) ;
#39858=AXIS2_PLACEMENT_3D ( 'NONE', #5760, #7098, #278 ) ;
#39894=ORIENTED_EDGE ( 'NONE', *, *, #56888, .F. ) ;
#39974=DIRECTION ( 'NONE',  ( 1.000000000000000000, 0.000000000000000000, 0.000000000000000000 ) ) ;
#39982=DIRECTION ( 'NONE',  ( 0.000000000000000000, -1.000000000000000000, 0.000000000000000000 ) ) ;
#40019=FACE_OUTER_BOUND ( 'NONE', #58658, .T. ) ;
#40033=VERTEX_POINT ( 'NONE', #12008 ) ;
#40100=CARTESIAN_POINT ( 'NONE',  ( -12.17631415595668010, 85.81613294202711018, 117.9291186787848176 ) ) ;
#40159=CLOSED_SHELL ( 'NONE', ( #57160, #40447, #39732, #45501, #17611, #45740, #48639, #33894, #4116, #5933, #81900, #62943, #39213, #38491, #7875, #60226, #79340, #38456, #9799, #29593, #18403, #77496, #86723, #59823, #67217, #80651, #30571, #15362, #74074, #53049, #82431, #66661, #71884, #30728, #56260, #64980, #56949, #17198, #79751, #63528, #41853, #23990, #70218, #21406, #84096, #65591, #77532, #6853, #52413, #35852, #68782, #50387, #33719, #47441, #5496, #16844, #70824, #10033, #37588, #49798, #66897, #3079, #23665, #89581, #23744, #12866, #60398, #49546, #80309, #78761, #7807, #79050, #9908, #17470, #21280, #10908, #29701, #21709, #69615, #32533, #80, #11919, #74192, #79254, #61720, #54771, #59647, #42591, #69553, #40234, #43514, #77419, #39154, #34835, #25182, #31038, #64332, #47599, #42933, #80479 ) ) ;
#40169=EDGE_CURVE ( 'NONE', #45628, #85065, #49183, .T. ) ;
#40172=CARTESIAN_POINT ( 'NONE',  ( 38.10000000000000142, 69.84999999999999432, 283.4005000000000223 ) ) ;
#40234=ADVANCED_FACE ( 'NONE', ( #55990, #78278 ), #70553, .F. ) ;
#40262=ORIENTED_EDGE ( 'NONE', *, *, #25998, .F. ) ;
#40295=EDGE_LOOP ( 'NONE', ( #5943, #72529, #21979, #22264 ) ) ;
#40319=CARTESIAN_POINT ( 'NONE',  ( 51.39690000000000225, 82.54999999999999716, 344.4418053999999643 ) ) ;
#40366=VERTEX_POINT ( 'NONE', #40823 ) ;
#40385=SHAPE_DEFINITION_REPRESENTATION ( #43964, #28740 ) ;
#40400=CIRCLE ( 'NONE', #73801, 6.858000000000003205 ) ;
#40416=ORIENTED_EDGE ( 'NONE', *, *, #53119, .T. ) ;
#40447=ADVANCED_FACE ( 'NONE', ( #69441 ), #82643, .F. ) ;
#40452=CARTESIAN_POINT ( 'NONE',  ( 34.92499999999999716, 66.67499999999999716, 292.1000000000000227 ) ) ;
#40507=DIRECTION ( 'NONE',  ( 0.000000000000000000, -1.000000000000000000, 0.000000000000000000 ) ) ;
#40557=DIRECTION ( 'NONE',  ( 0.000000000000000000, 0.000000000000000000, 1.000000000000000000 ) ) ;
#40565=FACE_OUTER_BOUND ( 'NONE', #15085, .T. ) ;
#40722=ORIENTED_EDGE ( 'NONE', *, *, #86004, .T. ) ;
#40767=EDGE_LOOP ( 'NONE', ( #60321, #86847, #81287, #37629 ) ) ;
#40796=EDGE_CURVE ( 'NONE', #31578, #12738, #82540, .T. ) ;
#40823=CARTESIAN_POINT ( 'NONE',  ( 52.38749999999999574, 94.53880000000000905, 229.3937500000000114 ) ) ;
#40827=ORIENTED_EDGE ( 'NONE', *, *, #27173, .F. ) ;
#40833=AXIS2_PLACEMENT_3D ( 'NONE', #45320, #9482, #2680 ) ;
#40875=CARTESIAN_POINT ( 'NONE',  ( 23.30821534676788787, 78.76419614706141203, 305.8009406276586333 ) ) ;
#40896=VECTOR ( 'NONE', #10706, 1000.000000000000000 ) ;
#40905=EDGE_LOOP ( 'NONE', ( #12355, #86620 ) ) ;
#40946=DIRECTION ( 'NONE',  ( 0.000000000000000000, 0.4999999999999994449, -0.8660254037844389297 ) ) ;
#40963=CARTESIAN_POINT ( 'NONE',  ( 44.45000000000000284, 69.84999999999999432, 219.0749999999999886 ) ) ;
#40995=VERTEX_POINT ( 'NONE', #65637 ) ;
#41020=CARTESIAN_POINT ( 'NONE',  ( 52.38749999999999574, 94.53880000000000905, 225.4249999999999829 ) ) ;
#41099=ORIENTED_EDGE ( 'NONE', *, *, #81656, .T. ) ;
#41108=ORIENTED_EDGE ( 'NONE', *, *, #77466, .T. ) ;
#41134=DIRECTION ( 'NONE',  ( -1.000000000000000000, 0.000000000000000000, 0.000000000000000000 ) ) ;
#41141=DIRECTION ( 'NONE',  ( 0.000000000000000000, 0.000000000000000000, -1.000000000000000000 ) ) ;
#41147=FACE_OUTER_BOUND ( 'NONE', #7212, .T. ) ;
#41158=DIRECTION ( 'NONE',  ( 0.000000000000000000, -1.000000000000000000, 0.000000000000000000 ) ) ;
#41165=ORIENTED_EDGE ( 'NONE', *, *, #73855, .T. ) ;
#41183=VECTOR ( 'NONE', #34579, 1000.000000000000000 ) ;
#41217=VERTEX_POINT ( 'NONE', #48747 ) ;
#41220=FACE_OUTER_BOUND ( 'NONE', #57075, .T. ) ;
#41326=VERTEX_POINT ( 'NONE', #82423 ) ;
#41342=AXIS2_PLACEMENT_3D ( 'NONE', #74099, #25498, #25955 ) ;
#41362=CARTESIAN_POINT ( 'NONE',  ( 74.98969683741650272, 82.54999999999999716, 346.9005000000000223 ) ) ;
#41371=AXIS2_PLACEMENT_3D ( 'NONE', #69514, #84048, #13649 ) ;
#41390=CONICAL_SURFACE ( 'NONE', #26879, 6.857999999999975671, 0.02993239667170383839 ) ;
#41415=DIRECTION ( 'NONE',  ( 1.000000000000000000, 0.000000000000000000, 0.000000000000000000 ) ) ;
#41435=CARTESIAN_POINT ( 'NONE',  ( -3.260447369053748545, 94.72788168350989224, 118.5118207592319379 ) ) ;
#41451=CIRCLE ( 'NONE', #13928, 3.174999999999983391 ) ;
#41516=ORIENTED_EDGE ( 'NONE', *, *, #51323, .F. ) ;
#41524=DIRECTION ( 'NONE',  ( 0.000000000000000000, -1.000000000000000000, 0.000000000000000000 ) ) ;
#41565=CARTESIAN_POINT ( 'NONE',  ( 57.14999999999999858, 95.25000000000000000, 323.0879999999999654 ) ) ;
#41590=DIRECTION ( 'NONE',  ( 1.000000000000000000, 0.000000000000000000, -9.299908063537909262E-17 ) ) ;
#41625=VECTOR ( 'NONE', #76864, 1000.000000000000000 ) ;
#41708=AXIS2_PLACEMENT_3D ( 'NONE', #7191, #75784, #74886 ) ;
#41739=ORIENTED_EDGE ( 'NONE', *, *, #21849, .F. ) ;
#41750=ORIENTED_EDGE ( 'NONE', *, *, #42602, .F. ) ;
#41813=AXIS2_PLACEMENT_3D ( 'NONE', #81191, #39380, #32111 ) ;
#41839=LINE ( 'NONE', #83215, #48967 ) ;
#41853=ADVANCED_FACE ( 'NONE', ( #46696 ), #10854, .T. ) ;
#41897=CIRCLE ( 'NONE', #28912, 3.000000000000002665 ) ;
#41918=DIRECTION ( 'NONE',  ( 0.000000000000000000, -1.000000000000000000, 0.000000000000000000 ) ) ;
#41926=DIRECTION ( 'NONE',  ( 0.000000000000000000, -1.000000000000000000, 0.000000000000000000 ) ) ;
#41970=EDGE_CURVE ( 'NONE', #74884, #56872, #38388, .T. ) ;
#41978=EDGE_LOOP ( 'NONE', ( #71236, #37594, #84351, #77786 ) ) ;
#41995=FACE_BOUND ( 'NONE', #49343, .T. ) ;
#42002=DIRECTION ( 'NONE',  ( 0.7071067811865474617, 0.000000000000000000, 0.7071067811865474617 ) ) ;
#42033=ORIENTED_EDGE ( 'NONE', *, *, #68571, .F. ) ;
#42102=EDGE_CURVE ( 'NONE', #24379, #21876, #53333, .T. ) ;
#42155=DIRECTION ( 'NONE',  ( 0.000000000000000000, 0.000000000000000000, 1.000000000000000000 ) ) ;
#42240=ORIENTED_EDGE ( 'NONE', *, *, #12443, .T. ) ;
#42256=DIRECTION ( 'NONE',  ( -1.784063995862374817E-16, 0.000000000000000000, -1.000000000000000000 ) ) ;
#42272=LINE ( 'NONE', #77266, #742 ) ;
#42288=ORIENTED_EDGE ( 'NONE', *, *, #19760, .F. ) ;
#42316=ORIENTED_EDGE ( 'NONE', *, *, #52583, .T. ) ;
#42380=ORIENTED_EDGE ( 'NONE', *, *, #80871, .F. ) ;
#42396=CIRCLE ( 'NONE', #13375, 3.000000000000002665 ) ;
#42452=VECTOR ( 'NONE', #17900, 1000.000000000000000 ) ;
#42518=ORIENTED_EDGE ( 'NONE', *, *, #59610, .T. ) ;
#42540=AXIS2_PLACEMENT_3D ( 'NONE', #6108, #70915, #49539 ) ;
#42541=FACE_OUTER_BOUND ( 'NONE', #13886, .T. ) ;
#42591=ADVANCED_FACE ( 'NONE', ( #13273 ), #49108, .F. ) ;
#42602=EDGE_CURVE ( 'NONE', #2492, #74022, #6453, .T. ) ;
#42615=EDGE_CURVE ( 'NONE', #82905, #64449, #30814, .T. ) ;
#42616=FACE_OUTER_BOUND ( 'NONE', #67025, .T. ) ;
#42670=CIRCLE ( 'NONE', #71693, 4.762500000000002842 ) ;
#42683=ORIENTED_EDGE ( 'NONE', *, *, #9802, .F. ) ;
#42724=CIRCLE ( 'NONE', #70305, 16.09746158385918946 ) ;
#42753=DIRECTION ( 'NONE',  ( 0.000000000000000000, 0.000000000000000000, 1.000000000000000000 ) ) ;
#42770=LINE ( 'NONE', #8284, #16329 ) ;
#42783=ORIENTED_EDGE ( 'NONE', *, *, #78215, .F. ) ;
#42802=VERTEX_POINT ( 'NONE', #20331 ) ;
#42817=DIRECTION ( 'NONE',  ( 0.000000000000000000, 0.000000000000000000, 1.000000000000000000 ) ) ;
#42861=LINE ( 'NONE', #43313, #1210 ) ;
#42909=( LENGTH_UNIT ( ) NAMED_UNIT ( * ) SI_UNIT ( .MILLI., .METRE. ) );
#42920=VECTOR ( 'NONE', #28685, 1000.000000000000000 ) ;
#42933=ADVANCED_FACE ( 'NONE', ( #11716 ), #44784, .T. ) ;
#42937=EDGE_CURVE ( 'NONE', #60387, #66434, #39409, .T. ) ;
#42998=CARTESIAN_POINT ( 'NONE',  ( -7.661254700127833495, 82.54999999999999716, 317.6630000000000109 ) ) ;
#43055=VECTOR ( 'NONE', #39982, 1000.000000000000000 ) ;
#43094=ORIENTED_EDGE ( 'NONE', *, *, #5310, .F. ) ;
#43105=CARTESIAN_POINT ( 'NONE',  ( 23.75871628398701318, 82.23350611626385387, 298.1325000000000500 ) ) ;
#43204=CARTESIAN_POINT ( 'NONE',  ( 23.62137175363338315, 84.66824784807761262, 298.6181131755103024 ) ) ;
#43229=ORIENTED_EDGE ( 'NONE', *, *, #66917, .F. ) ;
#43254=ORIENTED_EDGE ( 'NONE', *, *, #39427, .F. ) ;
#43313=CARTESIAN_POINT ( 'NONE',  ( 82.54999999999999716, 95.25000000000000000, 280.2255000000000109 ) ) ;
#43319=DIRECTION ( 'NONE',  ( 0.000000000000000000, 0.000000000000000000, 1.000000000000000000 ) ) ;
#43321=CARTESIAN_POINT ( 'NONE',  ( 4.829302083966705794, 70.89057043354831933, 118.4594231900968850 ) ) ;
#43324=EDGE_CURVE ( 'NONE', #74968, #50079, #86943, .T. ) ;
#43378=DIRECTION ( 'NONE',  ( 1.000000000000000000, 0.000000000000000000, 0.000000000000000000 ) ) ;
#43431=AXIS2_PLACEMENT_3D ( 'NONE', #39811, #41158, #67533 ) ;
#43505=VERTEX_POINT ( 'NONE', #72393 ) ;
#43514=ADVANCED_FACE ( 'NONE', ( #3348 ), #58731, .F. ) ;
#43601=ORIENTED_EDGE ( 'NONE', *, *, #58787, .F. ) ;
#43605=ORIENTED_EDGE ( 'NONE', *, *, #74093, .F. ) ;
#43756=VECTOR ( 'NONE', #16528, 1000.000000000000000 ) ;
#43905=EDGE_LOOP ( 'NONE', ( #32777, #39168 ) ) ;
#43957=VECTOR ( 'NONE', #42002, 1000.000000000000114 ) ;
#43964=PRODUCT_DEFINITION_SHAPE ( 'NONE', 'NONE',  #1182 ) ;
#44067=DIRECTION ( 'NONE',  ( 0.000000000000000000, 0.000000000000000000, 1.000000000000000000 ) ) ;
#44096=EDGE_CURVE ( 'NONE', #46935, #82352, #17432, .T. ) ;
#44122=DIRECTION ( 'NONE',  ( 0.000000000000000000, 0.000000000000000000, -1.000000000000000000 ) ) ;
#44130=ORIENTED_EDGE ( 'NONE', *, *, #76350, .F. ) ;
#44301=ORIENTED_EDGE ( 'NONE', *, *, #57401, .F. ) ;
#44327=FACE_OUTER_BOUND ( 'NONE', #85303, .T. ) ;
#44337=ORIENTED_EDGE ( 'NONE', *, *, #804, .F. ) ;
#44353=VERTEX_POINT ( 'NONE', #47675 ) ;
#44355=EDGE_CURVE ( 'NONE', #3897, #42802, #13088, .T. ) ;
#44365=ORIENTED_EDGE ( 'NONE', *, *, #22960, .T. ) ;
#44382=CARTESIAN_POINT ( 'NONE',  ( 6.938893903907229955E-15, 60.82030000000000314, 216.0269999999999868 ) ) ;
#44401=ORIENTED_EDGE ( 'NONE', *, *, #7301, .T. ) ;
#44461=EDGE_LOOP ( 'NONE', ( #28429, #2149, #78083, #7372 ) ) ;
#44479=CARTESIAN_POINT ( 'NONE',  ( 34.92499999999999716, 77.96728223830730542, 294.9574999999999818 ) ) ;
#44501=CARTESIAN_POINT ( 'NONE',  ( 38.10000000000000142, 82.54999999999999716, 290.4490000000000123 ) ) ;
#44533=CIRCLE ( 'NONE', #67764, 3.174999999999983391 ) ;
#44543=DIRECTION ( 'NONE',  ( -1.000000000000000000, -1.561055996379579722E-16, 0.000000000000000000 ) ) ;
#44548=ORIENTED_EDGE ( 'NONE', *, *, #34321, .T. ) ;
#44568=ADVANCED_BREP_SHAPE_REPRESENTATION ( '', ( #80246, #50656 ), #14432 ) ;
#44569=EDGE_CURVE ( 'NONE', #4499, #85158, #1346, .T. ) ;
#44596=CARTESIAN_POINT ( 'NONE',  ( 1.793207055312195196E-22, 69.95000000000000284, 118.5560000000000116 ) ) ;
#44657=CARTESIAN_POINT ( 'NONE',  ( 47.62500000000000000, 69.84999999999999432, 292.1000000000000227 ) ) ;
#44661=CARTESIAN_POINT ( 'NONE',  ( 6.299530400837946686, 71.63002361900261405, 118.3890773279586170 ) ) ;
#44666=CARTESIAN_POINT ( 'NONE',  ( -44.45000000000000284, 114.2999999999999972, 206.3750000000000000 ) ) ;
#44710=VECTOR ( 'NONE', #39088, 1000.000000000000000 ) ;
#44713=ORIENTED_EDGE ( 'NONE', *, *, #75022, .T. ) ;
#44765=EDGE_CURVE ( 'NONE', #72947, #59883, #32004, .T. ) ;
#44781=CARTESIAN_POINT ( 'NONE',  ( 44.45000000000000284, 69.84999999999999432, 219.0749999999999886 ) ) ;
#44784=TOROIDAL_SURFACE ( 'NONE', #46247, 13.09746158385919124, 3.000000000000000000 ) ;
#44795=VECTOR ( 'NONE', #23753, 999.9999999999998863 ) ;
#44796=LINE ( 'NONE', #72524, #69925 ) ;
#44891=CARTESIAN_POINT ( 'NONE',  ( 34.92499999999999716, 82.54999999999999716, 302.8950000000000387 ) ) ;
#44895=ORIENTED_EDGE ( 'NONE', *, *, #3577, .T. ) ;
#44906=ORIENTED_EDGE ( 'NONE', *, *, #77263, .T. ) ;
#44942=LINE ( 'NONE', #24079, #14934 ) ;
#44952=VERTEX_POINT ( 'NONE', #84708 ) ;
#44990=CARTESIAN_POINT ( 'NONE',  ( 23.30877932141580544, 86.33358099468556190, 299.9857356779602355 ) ) ;
#45033=PRESENTATION_STYLE_ASSIGNMENT (( #8422 ) ) ;
#45041=AXIS2_PLACEMENT_3D ( 'NONE', #24987, #19063, #19964 ) ;
#45047=AXIS2_PLACEMENT_3D ( 'NONE', #20050, #61366, #48174 ) ;
#45071=ORIENTED_EDGE ( 'NONE', *, *, #3123, .T. ) ;
#45091=CIRCLE ( 'NONE', #11791, 5.562600000000000655 ) ;
#45136=FACE_OUTER_BOUND ( 'NONE', #13443, .T. ) ;
#45147=EDGE_CURVE ( 'NONE', #47135, #27284, #46571, .T. ) ;
#45194=AXIS2_PLACEMENT_3D ( 'NONE', #71569, #31097, #17915 ) ;
#45198=EDGE_CURVE ( 'NONE', #70994, #56609, #19046, .T. ) ;
#45205=DIRECTION ( 'NONE',  ( 1.000000000000000000, 0.000000000000000000, -1.821231995776174986E-16 ) ) ;
#45216=PLANE ( 'NONE',  #48949 ) ;
#45260=EDGE_CURVE ( 'NONE', #85158, #52329, #45091, .T. ) ;
#45281=VERTEX_POINT ( 'NONE', #78274 ) ;
#45320=CARTESIAN_POINT ( 'NONE',  ( 44.45000000000000284, 69.84999999999999432, 219.0749999999999886 ) ) ;
#45325=EDGE_LOOP ( 'NONE', ( #77984, #38017, #54026, #68675, #22301 ) ) ;
#45335=DIRECTION ( 'NONE',  ( 1.000000000000000000, 0.000000000000000000, 1.248844797103662002E-15 ) ) ;
#45350=CARTESIAN_POINT ( 'NONE',  ( 88.90000000000000568, 66.67499999999999716, 342.8999999999999773 ) ) ;
#45462=CARTESIAN_POINT ( 'NONE',  ( 34.92499999999999716, 82.54999999999999716, 302.8950000000000387 ) ) ;
#45485=ORIENTED_EDGE ( 'NONE', *, *, #75533, .T. ) ;
#45493=DIRECTION ( 'NONE',  ( -1.000000000000000000, 0.000000000000000000, -9.713237310806269221E-16 ) ) ;
#45501=ADVANCED_FACE ( 'NONE', ( #17808 ), #74118, .T. ) ;
#45566=AXIS2_PLACEMENT_3D ( 'NONE', #68569, #27219, #48529 ) ;
#45598=DIRECTION ( 'NONE',  ( -0.8660254037844387076, -0.4999999999999998890, 0.000000000000000000 ) ) ;
#45621=ORIENTED_EDGE ( 'NONE', *, *, #62027, .T. ) ;
#45628=VERTEX_POINT ( 'NONE', #47285 ) ;
#45642=CARTESIAN_POINT ( 'NONE',  ( 47.62500000000000000, 73.02500000000000568, 219.0749999999999886 ) ) ;
#45652=DIRECTION ( 'NONE',  ( 0.000000000000000000, 0.000000000000000000, 1.000000000000000000 ) ) ;
#45656=DIRECTION ( 'NONE',  ( 0.000000000000000000, 0.000000000000000000, 1.000000000000000000 ) ) ;
#45731=CARTESIAN_POINT ( 'NONE',  ( 60.32499999999999574, 82.54999999999999716, 358.0130000000000337 ) ) ;
#45740=ADVANCED_FACE ( 'NONE', ( #35455, #953, #56341 ), #16822, .F. ) ;
#45870=LINE ( 'NONE', #73602, #70790 ) ;
#46079=FACE_OUTER_BOUND ( 'NONE', #76066, .T. ) ;
#46133=CARTESIAN_POINT ( 'NONE',  ( 34.92499999999999716, 87.13271776169270311, 294.9574999999999818 ) ) ;
#46144=CIRCLE ( 'NONE', #62118, 3.968749999999992895 ) ;
#46183=DIRECTION ( 'NONE',  ( 0.000000000000000000, 0.000000000000000000, -1.000000000000000000 ) ) ;
#46201=EDGE_CURVE ( 'NONE', #40366, #16110, #11913, .T. ) ;
#46247=AXIS2_PLACEMENT_3D ( 'NONE', #60737, #67117, #67566 ) ;
#46287=FACE_OUTER_BOUND ( 'NONE', #20986, .T. ) ;
#46288=VERTEX_POINT ( 'NONE', #71686 ) ;
#46353=LINE ( 'NONE', #74085, #17394 ) ;
#46427=ORIENTED_EDGE ( 'NONE', *, *, #55731, .T. ) ;
#46472=VERTEX_POINT ( 'NONE', #4428 ) ;
#46503=LINE ( 'NONE', #5650, #74756 ) ;
#46555=EDGE_CURVE ( 'NONE', #18695, #86161, #53428, .T. ) ;
#46571=CIRCLE ( 'NONE', #61053, 12.44600000000001216 ) ;
#46574=VERTEX_POINT ( 'NONE', #75708 ) ;
#46597=ORIENTED_EDGE ( 'NONE', *, *, #16500, .F. ) ;
#46632=ORIENTED_EDGE ( 'NONE', *, *, #24977, .T. ) ;
#46642=AXIS2_PLACEMENT_3D ( 'NONE', #15033, #77710, #30008 ) ;
#46696=FACE_OUTER_BOUND ( 'NONE', #49515, .T. ) ;
#46758=PLANE ( 'NONE',  #34047 ) ;
#46762=EDGE_LOOP ( 'NONE', ( #51240, #50509, #66197 ) ) ;
#46825=EDGE_LOOP ( 'NONE', ( #136, #12702, #18990, #47053 ) ) ;
#46831=CARTESIAN_POINT ( 'NONE',  ( -7.661254700127833495, 82.54999999999999716, 320.6630000000000109 ) ) ;
#46848=CARTESIAN_POINT ( 'NONE',  ( 7.661254700127822836, 98.64746158385918307, 275.4630000000000223 ) ) ;
#46869=EDGE_CURVE ( 'NONE', #15433, #16125, #293, .T. ) ;
#46878=AXIS2_PLACEMENT_3D ( 'NONE', #88689, #32344, #87335 ) ;
#46935=VERTEX_POINT ( 'NONE', #86555 ) ;
#46938=CIRCLE ( 'NONE', #9241, 6.557978799109520196 ) ;
#47016=DIRECTION ( 'NONE',  ( 0.000000000000000000, 1.000000000000000000, 0.000000000000000000 ) ) ;
#47041=DIRECTION ( 'NONE',  ( -0.000000000000000000, -0.000000000000000000, -1.000000000000000000 ) ) ;
#47048=DIRECTION ( 'NONE',  ( -1.000000000000000000, 0.000000000000000000, 0.000000000000000000 ) ) ;
#47053=ORIENTED_EDGE ( 'NONE', *, *, #3163, .F. ) ;
#47064=PLANE ( 'NONE',  #41813 ) ;
#47071=EDGE_CURVE ( 'NONE', #40995, #20045, #26871, .T. ) ;
#47110=EDGE_CURVE ( 'NONE', #41326, #58613, #49934, .T. ) ;
#47135=VERTEX_POINT ( 'NONE', #12816 ) ;
#47156=CARTESIAN_POINT ( 'NONE',  ( 57.14999999999999858, 95.25000000000000000, 329.4379999999999882 ) ) ;
#47157=CARTESIAN_POINT ( 'NONE',  ( 74.98969683741650272, 82.54999999999999716, 346.9005000000000223 ) ) ;
#47158=CARTESIAN_POINT ( 'NONE',  ( 44.45000000000000284, 114.2999999999999972, 257.1750000000000114 ) ) ;
#47196=FACE_OUTER_BOUND ( 'NONE', #14652, .T. ) ;
#47202=VERTEX_POINT ( 'NONE', #67150 ) ;
#47219=DIRECTION ( 'NONE',  ( 1.000000000000000000, 0.000000000000000000, 0.000000000000000000 ) ) ;
#47234=CARTESIAN_POINT ( 'NONE',  ( 23.49588678361623906, 79.64122941661595689, 306.6787378533616106 ) ) ;
#47246=ORIENTED_EDGE ( 'NONE', *, *, #5392, .T. ) ;
#47285=CARTESIAN_POINT ( 'NONE',  ( 38.10000000000000142, 69.84999999999999432, 292.1000000000000227 ) ) ;
#47299=DIRECTION ( 'NONE',  ( 0.000000000000000000, 0.000000000000000000, 1.000000000000000000 ) ) ;
#47354=DIRECTION ( 'NONE',  ( 1.000000000000000000, 0.000000000000000000, -9.299908063537909262E-17 ) ) ;
#47433=ORIENTED_EDGE ( 'NONE', *, *, #37987, .T. ) ;
#47441=ADVANCED_FACE ( 'NONE', ( #41220 ), #1257, .T. ) ;
#47519=VECTOR ( 'NONE', #79367, 1000.000000000000000 ) ;
#47526=ORIENTED_EDGE ( 'NONE', *, *, #25131, .T. ) ;
#47599=ADVANCED_FACE ( 'NONE', ( #47196 ), #68821, .T. ) ;
#47601=DIRECTION ( 'NONE',  ( 0.000000000000000000, 0.4999999999999998890, 0.8660254037844387076 ) ) ;
#47616=AXIS2_PLACEMENT_3D ( 'NONE', #67265, #12314, #59544 ) ;
#47621=ORIENTED_EDGE ( 'NONE', *, *, #24977, .F. ) ;
#47642=AXIS2_PLACEMENT_3D ( 'NONE', #48839, #35680, #7537 ) ;
#47675=CARTESIAN_POINT ( 'NONE',  ( 1.793207055312195196E-22, 69.95000000000000284, 118.5560000000000116 ) ) ;
#47683=CARTESIAN_POINT ( 'NONE',  ( 23.74957699733089100, 81.92546328272709388, 307.6268863596367851 ) ) ;
#47706=CARTESIAN_POINT ( 'NONE',  ( 38.10000000000000142, 69.84999999999999432, 283.4005000000000223 ) ) ;
#47733=CARTESIAN_POINT ( 'NONE',  ( -9.497924344318278145, 74.22888403371547383, 118.1764031952407663 ) ) ;
#47753=PLANE ( 'NONE',  #75517 ) ;
#47781=AXIS2_PLACEMENT_3D ( 'NONE', #2037, #15217, #78358 ) ;
#47800=AXIS2_PLACEMENT_3D ( 'NONE', #21727, #20383, #49399 ) ;
#47847=CIRCLE ( 'NONE', #49278, 3.174999999999983391 ) ;
#47866=ORIENTED_EDGE ( 'NONE', *, *, #58322, .T. ) ;
#47888=CIRCLE ( 'NONE', #8765, 3.174999999999983391 ) ;
#47962=CARTESIAN_POINT ( 'NONE',  ( 57.14999999999999858, 69.84999999999999432, 304.0379999999999541 ) ) ;
#47968=CARTESIAN_POINT ( 'NONE',  ( 28.57499999999999929, 87.13271776169258942, 310.8325000000000387 ) ) ;
#47972=DIRECTION ( 'NONE',  ( 0.000000000000000000, -1.000000000000000000, 0.000000000000000000 ) ) ;
#47992=CARTESIAN_POINT ( 'NONE',  ( 12.59999999999999964, 82.54999999999999716, 117.8845415480757595 ) ) ;
#48003=CARTESIAN_POINT ( 'NONE',  ( 34.92499999999999716, 66.67499999999999716, 342.8999999999999773 ) ) ;
#48033=VECTOR ( 'NONE', #42256, 1000.000000000000000 ) ;
#48045=CARTESIAN_POINT ( 'NONE',  ( 44.45000000000000284, 66.67499999999999716, 219.0749999999999886 ) ) ;
#48084=CARTESIAN_POINT ( 'NONE',  ( 47.62500000000000000, 94.53880000000000905, 221.4562499999999829 ) ) ;
#48165=AXIS2_PLACEMENT_3D ( 'NONE', #89324, #48390, #27527 ) ;
#48174=DIRECTION ( 'NONE',  ( 0.000000000000000000, 0.000000000000000000, -1.000000000000000000 ) ) ;
#48223=CARTESIAN_POINT ( 'NONE',  ( 28.57499999999999929, 77.96728223830740490, 310.8325000000000387 ) ) ;
#48311=CARTESIAN_POINT ( 'NONE',  ( 67.65734841870819594, 95.25000000000000000, 358.0130000000000337 ) ) ;
#48326=CARTESIAN_POINT ( 'NONE',  ( 44.45000000000000284, 69.84999999999999432, 288.9250000000000114 ) ) ;
#48328=EDGE_CURVE ( 'NONE', #35448, #79680, #10259, .T. ) ;
#48333=ORIENTED_EDGE ( 'NONE', *, *, #48328, .T. ) ;
#48390=DIRECTION ( 'NONE',  ( 0.000000000000000000, 1.000000000000000000, 0.000000000000000000 ) ) ;
#48426=ORIENTED_EDGE ( 'NONE', *, *, #80588, .T. ) ;
#48529=DIRECTION ( 'NONE',  ( 1.000000000000000000, 0.000000000000000000, 0.000000000000000000 ) ) ;
#48563=EDGE_CURVE ( 'NONE', #85065, #71100, #26125, .T. ) ;
#48568=CARTESIAN_POINT ( 'NONE',  ( 23.62126498357886462, 80.43107061863682361, 298.6185181214070212 ) ) ;
#48586=DIRECTION ( 'NONE',  ( -1.000000000000000000, 0.000000000000000000, 0.000000000000000000 ) ) ;
#48639=ADVANCED_FACE ( 'NONE', ( #70141, #77862 ), #22010, .F. ) ;
#48701=CYLINDRICAL_SURFACE ( 'NONE', #79936, 5.562600000000000655 ) ;
#48747=CARTESIAN_POINT ( 'NONE',  ( 0.000000000000000000, 50.79999999999999716, 258.6990000000000123 ) ) ;
#48777=DIRECTION ( 'NONE',  ( -1.000000000000000000, -1.092739197465703932E-16, 0.000000000000000000 ) ) ;
#48801=ORIENTED_EDGE ( 'NONE', *, *, #37751, .F. ) ;
#48839=CARTESIAN_POINT ( 'NONE',  ( 7.661254700127833495, 95.64746158385918307, 317.6630000000000109 ) ) ;
#48896=AXIS2_PLACEMENT_3D ( 'NONE', #48326, #5239, #54693 ) ;
#48949=AXIS2_PLACEMENT_3D ( 'NONE', #32484, #23477, #9834 ) ;
#48967=VECTOR ( 'NONE', #70477, 1000.000000000000000 ) ;
#49017=CARTESIAN_POINT ( 'NONE',  ( 23.35552145179432770, 78.96279258983980753, 299.7471977194603028 ) ) ;
#49028=EDGE_CURVE ( 'NONE', #10129, #32950, #12381, .T. ) ;
#49037=CARTESIAN_POINT ( 'NONE',  ( 38.10000000000000142, 69.84999999999999432, 358.0130000000000337 ) ) ;
#49094=FACE_OUTER_BOUND ( 'NONE', #30835, .T. ) ;
#49102=EDGE_LOOP ( 'NONE', ( #56276, #61736, #44401, #84285 ) ) ;
#49108=PLANE ( 'NONE',  #86880 ) ;
#49125=ORIENTED_EDGE ( 'NONE', *, *, #23659, .F. ) ;
#49138=EDGE_CURVE ( 'NONE', #43505, #55059, #34608, .T. ) ;
#49183=LINE ( 'NONE', #36482, #59040 ) ;
#49217=MECHANICAL_DESIGN_GEOMETRIC_PRESENTATION_REPRESENTATION('',(#26025),#57982);
#49229=DIRECTION ( 'NONE',  ( 1.092739197465703932E-16, -1.000000000000000000, 0.000000000000000000 ) ) ;
#49278=AXIS2_PLACEMENT_3D ( 'NONE', #30078, #85513, #30522 ) ;
#49324=VERTEX_POINT ( 'NONE', #78667 ) ;
#49339=ORIENTED_EDGE ( 'NONE', *, *, #86288, .F. ) ;
#49343=EDGE_LOOP ( 'NONE', ( #39682, #46427 ) ) ;
#49353=CARTESIAN_POINT ( 'NONE',  ( 57.14999999999999858, 95.25000000000000000, 280.2255000000000109 ) ) ;
#49399=DIRECTION ( 'NONE',  ( 1.000000000000000000, 0.000000000000000000, 0.000000000000000000 ) ) ;
#49415=CARTESIAN_POINT ( 'NONE',  ( 88.90000000000000568, 66.67499999999999716, 346.0750000000000455 ) ) ;
#49475=EDGE_CURVE ( 'NONE', #75348, #70994, #73599, .T. ) ;
#49515=EDGE_LOOP ( 'NONE', ( #55843, #27121, #490, #76457 ) ) ;
#49519=ORIENTED_EDGE ( 'NONE', *, *, #27231, .F. ) ;
#49535=CARTESIAN_POINT ( 'NONE',  ( 57.14999999999999858, 60.86974387893089755, 326.2630000000000337 ) ) ;
#49537=CIRCLE ( 'NONE', #64016, 3.174999999999983391 ) ;
#49539=DIRECTION ( 'NONE',  ( 0.000000000000000000, 1.000000000000000000, 0.000000000000000000 ) ) ;
#49546=ADVANCED_FACE ( 'NONE', ( #25906 ), #11379, .T. ) ;
#49551=AXIS2_PLACEMENT_3D ( 'NONE', #2761, #51766, #79515 ) ;
#49594=EDGE_CURVE ( 'NONE', #77147, #71100, #68133, .T. ) ;
#49595=CARTESIAN_POINT ( 'NONE',  ( 44.45000000000000284, 66.67499999999999716, 292.1000000000000227 ) ) ;
#49709=EDGE_CURVE ( 'NONE', #28060, #37074, #57527, .T. ) ;
#49732=SURFACE_SIDE_STYLE ('',( #247 ) ) ;
#49771=CARTESIAN_POINT ( 'NONE',  ( 51.39690000000000225, 82.54999999999999716, 335.3740053999999304 ) ) ;
#49781=PLANE ( 'NONE',  #35472 ) ;
#49785=ORIENTED_EDGE ( 'NONE', *, *, #82638, .T. ) ;
#49798=ADVANCED_FACE ( 'NONE', ( #72508 ), #79271, .F. ) ;
#49799=DIRECTION ( 'NONE',  ( 0.000000000000000000, -1.000000000000000000, 0.000000000000000000 ) ) ;
#49845=CARTESIAN_POINT ( 'NONE',  ( 7.669751788741939080, 92.55534477396975035, 118.3080865832529440 ) ) ;
#49934=CIRCLE ( 'NONE', #16564, 10.66800000000000459 ) ;
#49970=LINE ( 'NONE', #15488, #56287 ) ;
#49989=DIRECTION ( 'NONE',  ( 0.000000000000000000, -1.000000000000000000, 0.000000000000000000 ) ) ;
#50002=DIRECTION ( 'NONE',  ( 0.000000000000000000, 0.000000000000000000, -1.000000000000000000 ) ) ;
#50004=AXIS2_PLACEMENT_3D ( 'NONE', #25626, #53302, #81067 ) ;
#50058=ORIENTED_EDGE ( 'NONE', *, *, #3123, .F. ) ;
#50067=DIRECTION ( 'NONE',  ( -0.4999999999999998890, 0.8660254037844387076, 0.000000000000000000 ) ) ;
#50071=ORIENTED_EDGE ( 'NONE', *, *, #87576, .T. ) ;
#50079=VERTEX_POINT ( 'NONE', #22464 ) ;
#50126=VECTOR ( 'NONE', #19200, 999.9999999999998863 ) ;
#50147=AXIS2_PLACEMENT_3D ( 'NONE', #26430, #86873, #80066 ) ;
#50184=VERTEX_POINT ( 'NONE', #44666 ) ;
#50206=DIRECTION ( 'NONE',  ( -1.000000000000000000, 0.000000000000000000, 0.000000000000000000 ) ) ;
#50219=DIRECTION ( 'NONE',  ( -0.7071067811865420216, 0.000000000000000000, 0.7071067811865531239 ) ) ;
#50294=CARTESIAN_POINT ( 'NONE',  ( 11.93201035062058679, 86.61901526127904560, 117.9540879163301526 ) ) ;
#50326=ORIENTED_EDGE ( 'NONE', *, *, #76567, .T. ) ;
#50333=EDGE_CURVE ( 'NONE', #32579, #7668, #58993, .T. ) ;
#50376=EDGE_CURVE ( 'NONE', #56973, #65405, #7817, .T. ) ;
#50387=ADVANCED_FACE ( 'NONE', ( #69152 ), #63682, .T. ) ;
#50406=CIRCLE ( 'NONE', #24359, 3.968750000000020872 ) ;
#50501=EDGE_CURVE ( 'NONE', #64449, #56609, #13190, .T. ) ;
#50509=ORIENTED_EDGE ( 'NONE', *, *, #64836, .T. ) ;
#50558=EDGE_CURVE ( 'NONE', #22058, #31578, #25464, .T. ) ;
#50569=CARTESIAN_POINT ( 'NONE',  ( -44.45000000000000284, 50.79999999999999716, 257.1750000000000114 ) ) ;
#50588=CARTESIAN_POINT ( 'NONE',  ( 9.473969254672010010, 74.23277938464349290, 118.1771504636201797 ) ) ;
#50609=FACE_OUTER_BOUND ( 'NONE', #54397, .T. ) ;
#50615=FACE_OUTER_BOUND ( 'NONE', #33390, .T. ) ;
#50634=DIRECTION ( 'NONE',  ( 0.000000000000000000, 1.000000000000000000, 0.000000000000000000 ) ) ;
#50656=AXIS2_PLACEMENT_3D ( 'NONE', #89656, #19265, #5642 ) ;
#50744=VERTEX_POINT ( 'NONE', #35398 ) ;
#50755=CARTESIAN_POINT ( 'NONE',  ( 10.69948230274378531, 89.21725969999198469, 118.0724339613718570 ) ) ;
#50768=PLANE ( 'NONE',  #3560 ) ;
#50805=EDGE_CURVE ( 'NONE', #31593, #50744, #57652, .T. ) ;
#50837=VECTOR ( 'NONE', #75007, 1000.000000000000000 ) ;
#50968=AXIS2_PLACEMENT_3D ( 'NONE', #4959, #66272, #59007 ) ;
#50995=CARTESIAN_POINT ( 'NONE',  ( 52.99265158129170317, 95.25000000000000000, 346.9005000000000223 ) ) ;
#51017=CARTESIAN_POINT ( 'NONE',  ( 6.938893903907229955E-15, 50.79999999999999716, 210.4643999999999835 ) ) ;
#51026=EDGE_LOOP ( 'NONE', ( #89587, #33201, #24114, #77116 ) ) ;
#51039=CARTESIAN_POINT ( 'NONE',  ( 7.690721451477779524, 72.53503295708138410, 118.3083018788591971 ) ) ;
#51066=VERTEX_POINT ( 'NONE', #40319 ) ;
#51189=DIRECTION ( 'NONE',  ( 1.000000000000000000, 0.000000000000000000, 0.000000000000000000 ) ) ;
#51215=VECTOR ( 'NONE', #31728, 1000.000000000000000 ) ;
#51223=DIRECTION ( 'NONE',  ( -0.7071067811865420216, 0.000000000000000000, 0.7071067811865531239 ) ) ;
#51227=VERTEX_POINT ( 'NONE', #80639 ) ;
#51240=ORIENTED_EDGE ( 'NONE', *, *, #44569, .F. ) ;
#51323=EDGE_CURVE ( 'NONE', #53584, #70167, #24272, .T. ) ;
#51380=FACE_BOUND ( 'NONE', #86307, .T. ) ;
#51402=ORIENTED_EDGE ( 'NONE', *, *, #86310, .F. ) ;
#51470=CARTESIAN_POINT ( 'NONE',  ( 1.793207055312195196E-22, 69.95000000000000284, 118.5560000000000116 ) ) ;
#51519=AXIS2_PLACEMENT_3D ( 'NONE', #76788, #5971, #54518 ) ;
#51526=DIRECTION ( 'NONE',  ( 1.000000000000000000, 0.000000000000000000, -9.299908063537909262E-17 ) ) ;
#51536=PLANE ( 'NONE',  #12605 ) ;
#51552=CIRCLE ( 'NONE', #19657, 5.562599999999973122 ) ;
#51553=VECTOR ( 'NONE', #62300, 1000.000000000000000 ) ;
#51577=CARTESIAN_POINT ( 'NONE',  ( 47.62500000000000000, 66.67499999999999716, 288.9250000000000114 ) ) ;
#51595=ORIENTED_EDGE ( 'NONE', *, *, #75119, .T. ) ;
#51766=DIRECTION ( 'NONE',  ( 0.000000000000000000, 0.000000000000000000, 1.000000000000000000 ) ) ;
#51798=CARTESIAN_POINT ( 'NONE',  ( 23.44978778479566728, 85.69659655706036006, 306.4834544166336059 ) ) ;
#51801=EDGE_LOOP ( 'NONE', ( #37899, #23805, #81135, #6664 ) ) ;
#51826=PLANE ( 'NONE',  #33501 ) ;
#51891=AXIS2_PLACEMENT_3D ( 'NONE', #82805, #18762, #39643 ) ;
#51899=FACE_OUTER_BOUND ( 'NONE', #21755, .T. ) ;
#51955=EDGE_CURVE ( 'NONE', #17979, #52932, #10006, .T. ) ;
#52039=DIRECTION ( 'NONE',  ( 0.000000000000000000, 0.000000000000000000, -1.000000000000000000 ) ) ;
#52065=ORIENTED_EDGE ( 'NONE', *, *, #51955, .F. ) ;
#52099=DIRECTION ( 'NONE',  ( 0.000000000000000000, 0.000000000000000000, 1.000000000000000000 ) ) ;
#52120=COLOUR_RGB ( '', 0.66274510, 0.83137255, 0.94901961) ;
#52153=ORIENTED_EDGE ( 'NONE', *, *, #27231, .T. ) ;
#52154=LINE ( 'NONE', #58979, #10146 ) ;
#52195=ORIENTED_EDGE ( 'NONE', *, *, #44355, .T. ) ;
#52211=AXIS2_PLACEMENT_3D ( 'NONE', #66788, #59956, #39974 ) ;
#52233=CARTESIAN_POINT ( 'NONE',  ( 23.03812769098065161, 87.31235724081935246, 302.5802168940534216 ) ) ;
#52246=CARTESIAN_POINT ( 'NONE',  ( -23.75871628398702384, 82.54999999999999716, 275.4630000000000223 ) ) ;
#52286=CARTESIAN_POINT ( 'NONE',  ( -1.650252395058525057, 70.05163022878409151, 118.5452349891252339 ) ) ;
#52301=PLANE ( 'NONE',  #50147 ) ;
#52329=VERTEX_POINT ( 'NONE', #78063 ) ;
#52342=CARTESIAN_POINT ( 'NONE',  ( 60.32499999999999574, 82.54999999999999716, 358.0130000000000337 ) ) ;
#52374=CARTESIAN_POINT ( 'NONE',  ( 44.45000000000000284, 69.84999999999999432, 292.1000000000000227 ) ) ;
#52413=ADVANCED_FACE ( 'NONE', ( #26202 ), #47064, .F. ) ;
#52445=ORIENTED_EDGE ( 'NONE', *, *, #31013, .T. ) ;
#52583=EDGE_CURVE ( 'NONE', #79680, #60387, #44533, .T. ) ;
#52613=DIRECTION ( 'NONE',  ( 1.000000000000000000, 0.000000000000000000, -0.000000000000000000 ) ) ;
#52625=DIRECTION ( 'NONE',  ( 0.000000000000000000, -0.9995520592605569021, -0.02992792722492374630 ) ) ;
#52642=CARTESIAN_POINT ( 'NONE',  ( 7.661254700127822836, 98.64746158385918307, 317.6630000000000109 ) ) ;
#52646=CONICAL_SURFACE ( 'NONE', #46878, 10.66800000000000459, 0.02993239667170383839 ) ;
#52672=DIRECTION ( 'NONE',  ( 0.000000000000000000, 0.000000000000000000, 1.000000000000000000 ) ) ;
#52686=CARTESIAN_POINT ( 'NONE',  ( 0.000000000000000000, 50.79999999999999716, 265.5569999999999595 ) ) ;
#52732=ORIENTED_EDGE ( 'NONE', *, *, #7917, .T. ) ;
#52827=LINE ( 'NONE', #60118, #25513 ) ;
#52860=EDGE_LOOP ( 'NONE', ( #70457, #24927, #8005, #24216 ) ) ;
#52870=PLANE ( 'NONE',  #61371 ) ;
#52884=CARTESIAN_POINT ( 'NONE',  ( 34.92499999999999716, 82.54999999999999716, 302.8950000000000387 ) ) ;
#52897=CIRCLE ( 'NONE', #77605, 3.968749999999992895 ) ;
#52910=CARTESIAN_POINT ( 'NONE',  ( -7.661254700127833495, 66.45253841614081125, 320.6630000000000109 ) ) ;
#52932=VERTEX_POINT ( 'NONE', #12024 ) ;
#52951=CARTESIAN_POINT ( 'NONE',  ( 38.10000000000000142, 69.84999999999999432, 358.0130000000000337 ) ) ;
#52977=VERTEX_POINT ( 'NONE', #88782 ) ;
#53041=CARTESIAN_POINT ( 'NONE',  ( 6.349999999999999645, 82.54999999999999716, 302.8950000000000387 ) ) ;
#53049=ADVANCED_FACE ( 'NONE', ( #22311 ), #54656, .F. ) ;
#53068=ORIENTED_EDGE ( 'NONE', *, *, #6337, .F. ) ;
#53087=ORIENTED_EDGE ( 'NONE', *, *, #4672, .T. ) ;
#53108=DIRECTION ( 'NONE',  ( 0.000000000000000000, 0.000000000000000000, -1.000000000000000000 ) ) ;
#53119=EDGE_CURVE ( 'NONE', #17979, #53213, #23662, .T. ) ;
#53120=DIRECTION ( 'NONE',  ( -1.000000000000000000, 0.000000000000000000, 0.000000000000000000 ) ) ;
#53132=CYLINDRICAL_SURFACE ( 'NONE', #25823, 5.562599999999973122 ) ;
#53169=DIRECTION ( 'NONE',  ( 1.000000000000000000, 0.000000000000000000, 0.000000000000000000 ) ) ;
#53179=CARTESIAN_POINT ( 'NONE',  ( -6.309997437435098888, 71.63602457591818506, 118.3885225546303133 ) ) ;
#53206=EDGE_CURVE ( 'NONE', #79502, #51066, #10021, .T. ) ;
#53213=VERTEX_POINT ( 'NONE', #2767 ) ;
#53243=EDGE_LOOP ( 'NONE', ( #37808, #37329, #78863 ) ) ;
#53260=CARTESIAN_POINT ( 'NONE',  ( 50.79999999999999716, 73.02500000000000568, 219.0749999999999886 ) ) ;
#53302=DIRECTION ( 'NONE',  ( 1.000000000000000000, 0.000000000000000000, 0.000000000000000000 ) ) ;
#53327=VERTEX_POINT ( 'NONE', #48084 ) ;
#53333=LINE ( 'NONE', #40172, #66497 ) ;
#53355=ORIENTED_EDGE ( 'NONE', *, *, #86499, .F. ) ;
#53428=LINE ( 'NONE', #82094, #61239 ) ;
#53482=EDGE_CURVE ( 'NONE', #73971, #3897, #34919, .T. ) ;
#53550=EDGE_CURVE ( 'NONE', #79692, #14032, #46938, .T. ) ;
#53584=VERTEX_POINT ( 'NONE', #36729 ) ;
#53593=EDGE_CURVE ( 'NONE', #62569, #24379, #37169, .T. ) ;
#53633=CARTESIAN_POINT ( 'NONE',  ( -11.48301544705986998, 77.34703915398208096, 117.9986893718514409 ) ) ;
#53665=AXIS2_PLACEMENT_3D ( 'NONE', #77329, #70065, #71426 ) ;
#53682=CARTESIAN_POINT ( 'NONE',  ( 8.398627748552550652E-16, 50.79999999999999716, 272.4150000000000205 ) ) ;
#53708=VECTOR ( 'NONE', #86923, 1000.000000000000000 ) ;
#53821=DIRECTION ( 'NONE',  ( 0.000000000000000000, 1.000000000000000000, 0.000000000000000000 ) ) ;
#53872=EDGE_CURVE ( 'NONE', #72947, #47135, #54788, .T. ) ;
#53918=CARTESIAN_POINT ( 'NONE',  ( 57.14999999999999858, 95.25000000000000000, 326.2630000000000337 ) ) ;
#53960=DIRECTION ( 'NONE',  ( 0.000000000000000000, -1.000000000000000000, 0.000000000000000000 ) ) ;
#53971=ORIENTED_EDGE ( 'NONE', *, *, #57123, .F. ) ;
#53993=LINE ( 'NONE', #13149, #11873 ) ;
#53997=DIRECTION ( 'NONE',  ( 0.000000000000000000, 1.000000000000000000, 0.000000000000000000 ) ) ;
#54026=ORIENTED_EDGE ( 'NONE', *, *, #87288, .F. ) ;
#54033=CARTESIAN_POINT ( 'NONE',  ( 23.35562885956705514, 78.96316603869469475, 306.0434217894609787 ) ) ;
#54086=CARTESIAN_POINT ( 'NONE',  ( -11.95696095735741160, 78.49132214204263391, 117.9519267565928118 ) ) ;
#54109=CARTESIAN_POINT ( 'NONE',  ( 44.45000000000000284, 66.67499999999999716, 260.3500000000000227 ) ) ;
#54155=CARTESIAN_POINT ( 'NONE',  ( -8.316535683762193543, 92.02457483822063011, 118.2643808479089671 ) ) ;
#54164=CARTESIAN_POINT ( 'NONE',  ( 28.57499999999999929, 73.38456447661469895, 302.8950000000000387 ) ) ;
#54275=ORIENTED_EDGE ( 'NONE', *, *, #11328, .F. ) ;
#54344=EDGE_CURVE ( 'NONE', #34033, #70235, #1091, .T. ) ;
#54369=VERTEX_POINT ( 'NONE', #48311 ) ;
#54375=CARTESIAN_POINT ( 'NONE',  ( 44.45000000000000284, 66.67499999999999716, 288.9250000000000114 ) ) ;
#54380=ORIENTED_EDGE ( 'NONE', *, *, #46555, .T. ) ;
#54397=EDGE_LOOP ( 'NONE', ( #59595, #86282, #33054, #38758, #44365, #13965 ) ) ;
#54406=CARTESIAN_POINT ( 'NONE',  ( 85.72499999999999432, 66.67499999999999716, 342.8999999999999773 ) ) ;
#54428=DIRECTION ( 'NONE',  ( 0.000000000000000000, 0.000000000000000000, 1.000000000000000000 ) ) ;
#54452=FACE_OUTER_BOUND ( 'NONE', #25549, .T. ) ;
#54462=ORIENTED_EDGE ( 'NONE', *, *, #50501, .T. ) ;
#54466=AXIS2_PLACEMENT_3D ( 'NONE', #65438, #36403, #50002 ) ;
#54518=DIRECTION ( 'NONE',  ( 0.000000000000000000, 0.000000000000000000, 1.000000000000000000 ) ) ;
#54537=( NAMED_UNIT ( * ) SI_UNIT ( $, .STERADIAN. ) SOLID_ANGLE_UNIT ( ) );
#54552=DIRECTION ( 'NONE',  ( 1.000000000000000000, 0.000000000000000000, -9.299908063537909262E-17 ) ) ;
#54651=ORIENTED_EDGE ( 'NONE', *, *, #27816, .F. ) ;
#54656=PLANE ( 'NONE',  #42540 ) ;
#54661=CARTESIAN_POINT ( 'NONE',  ( 57.14999999999999858, 60.86974387893089755, 304.0379999999999541 ) ) ;
#54693=DIRECTION ( 'NONE',  ( 0.000000000000000000, 0.000000000000000000, -1.000000000000000000 ) ) ;
#54720=CIRCLE ( 'NONE', #35883, 3.174999999999983391 ) ;
#54758=LINE ( 'NONE', #25738, #517 ) ;
#54771=ADVANCED_FACE ( 'NONE', ( #60047 ), #52646, .F. ) ;
#54788=LINE ( 'NONE', #77508, #64354 ) ;
#54834=ORIENTED_EDGE ( 'NONE', *, *, #33393, .T. ) ;
#54846=VECTOR ( 'NONE', #30267, 1000.000000000000000 ) ;
#54893=PLANE ( 'NONE',  #33745 ) ;
#54913=EDGE_LOOP ( 'NONE', ( #86834, #57166, #86360, #56146, #42033 ) ) ;
#54928=CARTESIAN_POINT ( 'NONE',  ( 6.938893903907229955E-15, 50.79999999999999716, 216.0269999999999868 ) ) ;
#54934=VECTOR ( 'NONE', #55016, 1000.000000000000000 ) ;
#54946=DIRECTION ( 'NONE',  ( 0.000000000000000000, 0.000000000000000000, 1.000000000000000000 ) ) ;
#54976=LINE ( 'NONE', #28186, #50837 ) ;
#55016=DIRECTION ( 'NONE',  ( -0.000000000000000000, -0.000000000000000000, -1.000000000000000000 ) ) ;
#55042=FACE_OUTER_BOUND ( 'NONE', #70828, .T. ) ;
#55053=CARTESIAN_POINT ( 'NONE',  ( -4.052637573187175768, 94.48764834648464728, 118.4873761436849691 ) ) ;
#55059=VERTEX_POINT ( 'NONE', #36407 ) ;
#55060=CARTESIAN_POINT ( 'NONE',  ( 6.938893903907229955E-15, 50.79999999999999716, 216.0269999999999868 ) ) ;
#55076=CYLINDRICAL_SURFACE ( 'NONE', #88845, 8.928100000000000591 ) ;
#55085=DIRECTION ( 'NONE',  ( 1.000000000000000000, 0.000000000000000000, 0.000000000000000000 ) ) ;
#55154=EDGE_LOOP ( 'NONE', ( #44713, #52445, #59473, #42518 ) ) ;
#55192=VECTOR ( 'NONE', #8155, 999.9999999999998863 ) ;
#55207=ORIENTED_EDGE ( 'NONE', *, *, #61295, .F. ) ;
#55214=VECTOR ( 'NONE', #64539, 1000.000000000000000 ) ;
#55226=DIRECTION ( 'NONE',  ( 0.000000000000000000, 0.000000000000000000, -1.000000000000000000 ) ) ;
#55253=CARTESIAN_POINT ( 'NONE',  ( 28.57499999999999929, 91.71543552338529537, 302.8950000000000387 ) ) ;
#55285=ORIENTED_EDGE ( 'NONE', *, *, #10308, .F. ) ;
#55382=CARTESIAN_POINT ( 'NONE',  ( 23.68703819316727888, 81.00531446394714408, 298.3792380957531236 ) ) ;
#55391=DIRECTION ( 'NONE',  ( 0.000000000000000000, 1.000000000000000000, 0.000000000000000000 ) ) ;
#55475=CARTESIAN_POINT ( 'NONE',  ( 52.38749999999999574, 94.53880000000000905, 246.8562499999999886 ) ) ;
#55491=CARTESIAN_POINT ( 'NONE',  ( 60.32499999999999574, 82.54999999999999716, 335.3740053999999304 ) ) ;
#55619=VECTOR ( 'NONE', #64430, 1000.000000000000000 ) ;
#55627=FILL_AREA_STYLE_COLOUR ( '', #83451 ) ;
#55633=ORIENTED_EDGE ( 'NONE', *, *, #78516, .T. ) ;
#55660=CARTESIAN_POINT ( 'NONE',  ( 34.92499999999999716, 66.67499999999999716, 342.8999999999999773 ) ) ;
#55662=FACE_OUTER_BOUND ( 'NONE', #29981, .T. ) ;
#55702=CARTESIAN_POINT ( 'NONE',  ( 74.98969683741650272, 82.54999999999999716, 358.0130000000000337 ) ) ;
#55707=DIRECTION ( 'NONE',  ( 0.000000000000000000, 0.000000000000000000, 1.000000000000000000 ) ) ;
#55731=EDGE_CURVE ( 'NONE', #65405, #85819, #42670, .T. ) ;
#55743=CARTESIAN_POINT ( 'NONE',  ( 57.14999999999999858, 95.25000000000000000, 300.8629999999999995 ) ) ;
#55807=EDGE_CURVE ( 'NONE', #70994, #61646, #77034, .T. ) ;
#55841=ORIENTED_EDGE ( 'NONE', *, *, #49138, .F. ) ;
#55843=ORIENTED_EDGE ( 'NONE', *, *, #50376, .F. ) ;
#55848=LINE ( 'NONE', #40452, #72687 ) ;
#55870=DIRECTION ( 'NONE',  ( 0.000000000000000000, 1.000000000000000000, 0.000000000000000000 ) ) ;
#55886=VECTOR ( 'NONE', #11718, 1000.000000000000000 ) ;
#55892=VECTOR ( 'NONE', #84772, 1000.000000000000000 ) ;
#55913=DIRECTION ( 'NONE',  ( -1.000000000000000000, -5.782411586589351722E-16, 5.782411586589351722E-16 ) ) ;
#55929=CIRCLE ( 'NONE', #7904, 6.557978799109520196 ) ;
#55932=CARTESIAN_POINT ( 'NONE',  ( 7.620115932400929327E-15, 50.79999999999999716, 221.5895999999999901 ) ) ;
#55966=DIRECTION ( 'NONE',  ( 0.000000000000000000, 0.000000000000000000, 1.000000000000000000 ) ) ;
#55990=FACE_OUTER_BOUND ( 'NONE', #18440, .T. ) ;
#55995=DIRECTION ( 'NONE',  ( 1.248844797103662002E-15, 0.000000000000000000, -1.000000000000000000 ) ) ;
#56146=ORIENTED_EDGE ( 'NONE', *, *, #15955, .F. ) ;
#56202=CARTESIAN_POINT ( 'NONE',  ( 1.651468531095106718, 95.06824417558520679, 118.5472321064814452 ) ) ;
#56206=DIRECTION ( 'NONE',  ( 1.000000000000000000, 0.000000000000000000, 0.000000000000000000 ) ) ;
#56260=ADVANCED_FACE ( 'NONE', ( #32424 ), #60127, .F. ) ;
#56276=ORIENTED_EDGE ( 'NONE', *, *, #15758, .T. ) ;
#56287=VECTOR ( 'NONE', #70899, 1000.000000000000000 ) ;
#56303=FACE_BOUND ( 'NONE', #66562, .T. ) ;
#56319=EDGE_CURVE ( 'NONE', #1129, #68410, #14698, .T. ) ;
#56331=EDGE_CURVE ( 'NONE', #74022, #7823, #81936, .T. ) ;
#56341=FACE_BOUND ( 'NONE', #34702, .T. ) ;
#56342=ORIENTED_EDGE ( 'NONE', *, *, #86310, .T. ) ;
#56363=LINE ( 'NONE', #35927, #71253 ) ;
#56422=EDGE_LOOP ( 'NONE', ( #65693, #47433, #64165, #1035, #10524, #44548, #29496, #17004, #89137, #13079 ) ) ;
#56434=LINE ( 'NONE', #21950, #23814 ) ;
#56435=CARTESIAN_POINT ( 'NONE',  ( 7.661254700127844153, 66.45253841614081125, 320.6630000000000109 ) ) ;
#56558=ORIENTED_EDGE ( 'NONE', *, *, #87576, .F. ) ;
#56609=VERTEX_POINT ( 'NONE', #89102 ) ;
#56661=EDGE_LOOP ( 'NONE', ( #68035, #7178, #58777, #88674 ) ) ;
#56675=EDGE_CURVE ( 'NONE', #1395, #39002, #42272, .T. ) ;
#56691=ORIENTED_EDGE ( 'NONE', *, *, #2915, .T. ) ;
#56728=CARTESIAN_POINT ( 'NONE',  ( 57.14999999999999858, 69.84999999999999432, 300.8629999999999995 ) ) ;
#56836=LINE ( 'NONE', #55932, #6898 ) ;
#56865=DIRECTION ( 'NONE',  ( -0.000000000000000000, 1.000000000000000000, -0.000000000000000000 ) ) ;
#56872=VERTEX_POINT ( 'NONE', #10771 ) ;
#56886=CARTESIAN_POINT ( 'NONE',  ( 38.10000000000000142, 95.25000000000000000, 346.9005000000000223 ) ) ;
#56888=EDGE_CURVE ( 'NONE', #39002, #12424, #21035, .T. ) ;
#56899=CARTESIAN_POINT ( 'NONE',  ( 6.938893903907229955E-15, 67.86880000000000734, 216.0269999999999868 ) ) ;
#56949=ADVANCED_FACE ( 'NONE', ( #68887 ), #83414, .F. ) ;
#56956=EDGE_LOOP ( 'NONE', ( #14275, #33115, #6258, #9457, #16733 ) ) ;
#56973=VERTEX_POINT ( 'NONE', #75706 ) ;
#57031=CARTESIAN_POINT ( 'NONE',  ( 44.45000000000000284, 50.79999999999999716, 275.4630000000000223 ) ) ;
#57037=CARTESIAN_POINT ( 'NONE',  ( 0.000000000000000000, 60.82030000000000314, 265.5569999999999595 ) ) ;
#57075=EDGE_LOOP ( 'NONE', ( #82187, #34539, #41099, #72930 ) ) ;
#57093=FACE_BOUND ( 'NONE', #1947, .T. ) ;
#57106=CARTESIAN_POINT ( 'NONE',  ( 4.442782598225926805, 94.34796714030134979, 118.4733406123303610 ) ) ;
#57115=DIRECTION ( 'NONE',  ( -1.000000000000000000, 0.000000000000000000, 0.000000000000000000 ) ) ;
#57118=CARTESIAN_POINT ( 'NONE',  ( 44.45000000000000284, 66.67499999999999716, 257.1750000000000114 ) ) ;
#57123=EDGE_CURVE ( 'NONE', #46574, #75933, #85667, .T. ) ;
#57135=AXIS2_PLACEMENT_3D ( 'NONE', #68506, #7177, #62125 ) ;
#57144=DIRECTION ( 'NONE',  ( 0.000000000000000000, -1.000000000000000000, 0.000000000000000000 ) ) ;
#57160=ADVANCED_FACE ( 'NONE', ( #21650 ), #22601, .T. ) ;
#57166=ORIENTED_EDGE ( 'NONE', *, *, #59195, .T. ) ;
#57170=CIRCLE ( 'NONE', #68799, 5.562599999999973122 ) ;
#57197=DIRECTION ( 'NONE',  ( 0.000000000000000000, -1.000000000000000000, 0.000000000000000000 ) ) ;
#57220=LINE ( 'NONE', #78603, #29838 ) ;
#57283=CARTESIAN_POINT ( 'NONE',  ( 23.75871628398702384, 82.70597876660713155, 307.6575000000001410 ) ) ;
#57300=CARTESIAN_POINT ( 'NONE',  ( 44.45000000000000284, 66.67499999999999716, 257.1750000000000114 ) ) ;
#57301=ORIENTED_EDGE ( 'NONE', *, *, #47071, .F. ) ;
#57401=EDGE_CURVE ( 'NONE', #28060, #46472, #25643, .T. ) ;
#57403=CARTESIAN_POINT ( 'NONE',  ( 5.572218945471783869, 71.24158085953891373, 118.4255381658035020 ) ) ;
#57425=LINE ( 'NONE', #30177, #9947 ) ;
#57466=FACE_OUTER_BOUND ( 'NONE', #51026, .T. ) ;
#57488=DIRECTION ( 'NONE',  ( 0.000000000000000000, 0.000000000000000000, 1.000000000000000000 ) ) ;
#57493=DIRECTION ( 'NONE',  ( 0.000000000000000000, 0.000000000000000000, 1.000000000000000000 ) ) ;
#57527=CIRCLE ( 'NONE', #89446, 3.174999999999983391 ) ;
#57562=CARTESIAN_POINT ( 'NONE',  ( 12.17234669811228720, 85.83081271406847179, 117.9295285458294273 ) ) ;
#57577=FACE_OUTER_BOUND ( 'NONE', #28572, .T. ) ;
#57582=ORIENTED_EDGE ( 'NONE', *, *, #51955, .T. ) ;
#57652=CIRCLE ( 'NONE', #35868, 6.858000000000003205 ) ;
#57654=AXIS2_PLACEMENT_3D ( 'NONE', #87920, #45656, #73387 ) ;
#57676=DIRECTION ( 'NONE',  ( -1.000000000000000000, 0.000000000000000000, -0.000000000000000000 ) ) ;
#57741=CARTESIAN_POINT ( 'NONE',  ( 23.08500427215554751, 87.15872157593996405, 304.1353934756002104 ) ) ;
#57803=( NAMED_UNIT ( * ) SI_UNIT ( $, .STERADIAN. ) SOLID_ANGLE_UNIT ( ) );
#57876=DIRECTION ( 'NONE',  ( 1.000000000000000000, 0.000000000000000000, 0.000000000000000000 ) ) ;
#57898=CARTESIAN_POINT ( 'NONE',  ( 7.661254700127822836, 95.64746158385918307, 320.6630000000000109 ) ) ;
#57955=CARTESIAN_POINT ( 'NONE',  ( 12.59999999999999964, 82.54999999999999716, 206.3750000000000000 ) ) ;
#57956=FACE_OUTER_BOUND ( 'NONE', #51801, .T. ) ;
#57982=( GEOMETRIC_REPRESENTATION_CONTEXT ( 3 ) GLOBAL_UNCERTAINTY_ASSIGNED_CONTEXT ( ( #84191 ) ) GLOBAL_UNIT_ASSIGNED_CONTEXT ( ( #19161, #33680, #54537 ) ) REPRESENTATION_CONTEXT ( 'NONE', 'WORKASPACE' ) );
#58019=CARTESIAN_POINT ( 'NONE',  ( 52.38749999999999574, 94.53880000000000905, 250.8250000000000171 ) ) ;
#58030=DIRECTION ( 'NONE',  ( 0.000000000000000000, 0.000000000000000000, 1.000000000000000000 ) ) ;
#58139=VECTOR ( 'NONE', #7890, 999.9999999999998863 ) ;
#58167=VECTOR ( 'NONE', #63058, 1000.000000000000000 ) ;
#58189=CARTESIAN_POINT ( 'NONE',  ( 23.03803956593629465, 87.31264177286587369, 303.2054484439112798 ) ) ;
#58304=DIRECTION ( 'NONE',  ( 0.000000000000000000, 0.000000000000000000, 1.000000000000000000 ) ) ;
#58322=EDGE_CURVE ( 'NONE', #89263, #20045, #24988, .T. ) ;
#58378=DIRECTION ( 'NONE',  ( 1.000000000000000000, 0.000000000000000000, 0.000000000000000000 ) ) ;
#58381=DIRECTION ( 'NONE',  ( 1.000000000000000000, 0.000000000000000000, -0.000000000000000000 ) ) ;
#58464=DIRECTION ( 'NONE',  ( 1.000000000000000000, 0.000000000000000000, -1.821231995776179916E-16 ) ) ;
#58484=ORIENTED_EDGE ( 'NONE', *, *, #53482, .F. ) ;
#58529=CARTESIAN_POINT ( 'NONE',  ( 23.75871628398702384, 82.54999999999999716, 298.1325000000000500 ) ) ;
#58583=PLANE ( 'NONE',  #49551 ) ;
#58592=EDGE_CURVE ( 'NONE', #85819, #65405, #38450, .T. ) ;
#58613=VERTEX_POINT ( 'NONE', #39834 ) ;
#58654=EDGE_LOOP ( 'NONE', ( #13637, #53355 ) ) ;
#58658=EDGE_LOOP ( 'NONE', ( #50326, #52065, #40416, #4033, #71404, #16424, #56558 ) ) ;
#58731=CYLINDRICAL_SURFACE ( 'NONE', #62350, 8.928100000000000591 ) ;
#58767=ORIENTED_EDGE ( 'NONE', *, *, #41970, .F. ) ;
#58777=ORIENTED_EDGE ( 'NONE', *, *, #29398, .T. ) ;
#58787=EDGE_CURVE ( 'NONE', #6408, #74884, #63316, .T. ) ;
#58863=DIRECTION ( 'NONE',  ( 0.000000000000000000, 0.000000000000000000, 1.000000000000000000 ) ) ;
#58960=ORIENTED_EDGE ( 'NONE', *, *, #70932, .F. ) ;
#58979=CARTESIAN_POINT ( 'NONE',  ( 82.54999999999999716, 95.25000000000000000, 346.9005000000000223 ) ) ;
#58993=CIRCLE ( 'NONE', #9676, 3.174999999999983391 ) ;
#59007=DIRECTION ( 'NONE',  ( 0.000000000000000000, 0.000000000000000000, 1.000000000000000000 ) ) ;
#59015=CARTESIAN_POINT ( 'NONE',  ( 34.92499999999999716, 69.84999999999999432, 342.8999999999999773 ) ) ;
#59037=DIRECTION ( 'NONE',  ( 0.000000000000000000, 0.000000000000000000, -1.000000000000000000 ) ) ;
#59040=VECTOR ( 'NONE', #64187, 1000.000000000000000 ) ;
#59131=CARTESIAN_POINT ( 'NONE',  ( -23.75871628398702384, 82.54999999999999716, 320.6630000000000109 ) ) ;
#59139=EDGE_CURVE ( 'NONE', #45628, #84598, #34597, .T. ) ;
#59193=EDGE_CURVE ( 'NONE', #89263, #24990, #15064, .T. ) ;
#59195=EDGE_CURVE ( 'NONE', #40033, #80239, #15517, .T. ) ;
#59207=EDGE_CURVE ( 'NONE', #77463, #69696, #27784, .T. ) ;
#59228=LINE ( 'NONE', #80149, #42452 ) ;
#59250=FACE_OUTER_BOUND ( 'NONE', #26700, .T. ) ;
#59267=AXIS2_PLACEMENT_3D ( 'NONE', #71811, #9581, #62742 ) ;
#59427=ORIENTED_EDGE ( 'NONE', *, *, #50805, .T. ) ;
#59438=DIRECTION ( 'NONE',  ( 1.000000000000000000, 0.000000000000000000, -1.821231995776174986E-16 ) ) ;
#59473=ORIENTED_EDGE ( 'NONE', *, *, #22747, .F. ) ;
#59498=DIRECTION ( 'NONE',  ( 0.000000000000000000, 0.000000000000000000, -1.000000000000000000 ) ) ;
#59532=ORIENTED_EDGE ( 'NONE', *, *, #19760, .T. ) ;
#59544=DIRECTION ( 'NONE',  ( 1.000000000000000000, 0.000000000000000000, 0.000000000000000000 ) ) ;
#59545=AXIS2_PLACEMENT_3D ( 'NONE', #44891, #24468, #87142 ) ;
#59576=CARTESIAN_POINT ( 'NONE',  ( 44.45000000000000284, 114.2999999999999972, 275.4630000000000223 ) ) ;
#59577=PLANE ( 'NONE',  #12190 ) ;
#59586=CARTESIAN_POINT ( 'NONE',  ( 57.14999999999999858, 69.84999999999999432, 329.4379999999999882 ) ) ;
#59595=ORIENTED_EDGE ( 'NONE', *, *, #65936, .T. ) ;
#59610=EDGE_CURVE ( 'NONE', #81285, #23386, #83552, .T. ) ;
#59647=ADVANCED_FACE ( 'NONE', ( #62646, #22225 ), #14512, .T. ) ;
#59656=CARTESIAN_POINT ( 'NONE',  ( 31.75000000000000000, 69.84999999999999432, 292.1000000000000227 ) ) ;
#59727=LINE ( 'NONE', #2567, #54846 ) ;
#59761=VERTEX_POINT ( 'NONE', #31420 ) ;
#59812=EDGE_CURVE ( 'NONE', #44353, #69843, #34527, .T. ) ;
#59823=ADVANCED_FACE ( 'NONE', ( #32773, #67748 ), #74114, .F. ) ;
#59839=CARTESIAN_POINT ( 'NONE',  ( 44.45000000000000284, 111.1250000000000000, 257.1750000000000114 ) ) ;
#59860=DIRECTION ( 'NONE',  ( 1.000000000000000000, 1.092739197465703932E-16, 0.000000000000000000 ) ) ;
#59880=DIRECTION ( 'NONE',  ( 1.000000000000000000, 0.000000000000000000, 0.000000000000000000 ) ) ;
#59883=VERTEX_POINT ( 'NONE', #950 ) ;
#59939=EDGE_LOOP ( 'NONE', ( #797, #49519 ) ) ;
#59956=DIRECTION ( 'NONE',  ( 0.000000000000000000, 0.000000000000000000, 1.000000000000000000 ) ) ;
#59976=ORIENTED_EDGE ( 'NONE', *, *, #24105, .F. ) ;
#59998=CARTESIAN_POINT ( 'NONE',  ( 44.45000000000000284, 66.67499999999999716, 219.0749999999999886 ) ) ;
#60011=DIRECTION ( 'NONE',  ( -1.000000000000000000, 0.000000000000000000, 0.000000000000000000 ) ) ;
#60016=SURFACE_SIDE_STYLE ('',( #26860 ) ) ;
#60047=FACE_OUTER_BOUND ( 'NONE', #60120, .T. ) ;
#60053=CARTESIAN_POINT ( 'NONE',  ( 28.57499999999999929, 77.96728223830730542, 294.9574999999999818 ) ) ;
#60078=ORIENTED_EDGE ( 'NONE', *, *, #4477, .T. ) ;
#60118=CARTESIAN_POINT ( 'NONE',  ( 7.661254700127822836, 98.64746158385918307, 320.6630000000000109 ) ) ;
#60120=EDGE_LOOP ( 'NONE', ( #69724, #72422, #52153, #65833 ) ) ;
#60127=PLANE ( 'NONE',  #50004 ) ;
#60175=AXIS2_PLACEMENT_3D ( 'NONE', #34352, #7113, #5772 ) ;
#60176=DIRECTION ( 'NONE',  ( -1.821231995776179916E-16, 0.000000000000000000, -1.000000000000000000 ) ) ;
#60199=STYLED_ITEM ( 'NONE', ( #45033 ), #80246 ) ;
#60226=ADVANCED_FACE ( 'NONE', ( #33451 ), #14370, .F. ) ;
#60243=CARTESIAN_POINT ( 'NONE',  ( 88.90000000000000568, 69.84999999999999432, 219.0749999999999886 ) ) ;
#60275=DIRECTION ( 'NONE',  ( 1.000000000000000000, 0.000000000000000000, 0.000000000000000000 ) ) ;
#60321=ORIENTED_EDGE ( 'NONE', *, *, #866, .T. ) ;
#60387=VERTEX_POINT ( 'NONE', #25631 ) ;
#60398=ADVANCED_FACE ( 'NONE', ( #59250 ), #51536, .T. ) ;
#60403=EDGE_CURVE ( 'NONE', #23386, #45281, #10223, .T. ) ;
#60418=CARTESIAN_POINT ( 'NONE',  ( 23.75871628398702740, 82.23812670290168114, 307.6575000000000841 ) ) ;
#60465=CARTESIAN_POINT ( 'NONE',  ( -5.580972532898796246, 71.24585594549820655, 118.4251286083983246 ) ) ;
#60477=FACE_OUTER_BOUND ( 'NONE', #55154, .T. ) ;
#60538=CARTESIAN_POINT ( 'NONE',  ( -10.91960930477692671, 88.85017151735789298, 118.0522144908983933 ) ) ;
#60551=ORIENTED_EDGE ( 'NONE', *, *, #70981, .T. ) ;
#60553=CARTESIAN_POINT ( 'NONE',  ( 6.938893903907229955E-15, 67.86880000000000734, 210.4643999999999835 ) ) ;
#60566=LINE ( 'NONE', #11545, #10506 ) ;
#60642=FACE_OUTER_BOUND ( 'NONE', #31282, .T. ) ;
#60737=CARTESIAN_POINT ( 'NONE',  ( 7.661254700127833495, 82.54999999999999716, 317.6630000000000109 ) ) ;
#60792=VECTOR ( 'NONE', #81669, 1000.000000000000000 ) ;
#60877=CARTESIAN_POINT ( 'NONE',  ( 23.62182483554943957, 80.43530414067632250, 307.1735616208110855 ) ) ;
#60907=ORIENTED_EDGE ( 'NONE', *, *, #82841, .F. ) ;
#60915=PLANE ( 'NONE',  #27232 ) ;
#60926=CARTESIAN_POINT ( 'NONE',  ( -10.91422816413673402, 76.24044119408891618, 118.0527134162828276 ) ) ;
#61053=AXIS2_PLACEMENT_3D ( 'NONE', #19219, #75077, #13305 ) ;
#61089=CARTESIAN_POINT ( 'NONE',  ( -7.661254700127833495, 66.45253841614081125, 317.6630000000000109 ) ) ;
#61100=LINE ( 'NONE', #26583, #80888 ) ;
#61166=CARTESIAN_POINT ( 'NONE',  ( 44.45000000000000284, 66.67499999999999716, 260.3500000000000227 ) ) ;
#61218=DIRECTION ( 'NONE',  ( -1.092739197465703932E-16, 1.000000000000000000, 0.000000000000000000 ) ) ;
#61239=VECTOR ( 'NONE', #47972, 1000.000000000000000 ) ;
#61258=DIRECTION ( 'NONE',  ( 0.000000000000000000, 0.000000000000000000, -1.000000000000000000 ) ) ;
#61287=DIRECTION ( 'NONE',  ( 0.000000000000000000, -1.000000000000000000, 0.000000000000000000 ) ) ;
#61295=EDGE_CURVE ( 'NONE', #37074, #69509, #35464, .T. ) ;
#61308=CARTESIAN_POINT ( 'NONE',  ( 38.10000000000000142, 69.84999999999999432, 346.9005000000000223 ) ) ;
#61311=DIRECTION ( 'NONE',  ( 0.000000000000000000, -1.000000000000000000, 0.000000000000000000 ) ) ;
#61319=DIRECTION ( 'NONE',  ( 0.000000000000000000, -1.000000000000000000, 0.000000000000000000 ) ) ;
#61366=DIRECTION ( 'NONE',  ( 0.000000000000000000, 1.000000000000000000, 0.000000000000000000 ) ) ;
#61367=CARTESIAN_POINT ( 'NONE',  ( 5.562599999999999767, 60.82030000000000314, 265.5569999999999595 ) ) ;
#61371=AXIS2_PLACEMENT_3D ( 'NONE', #11133, #87896, #26119 ) ;
#61381=EDGE_LOOP ( 'NONE', ( #30353, #7416, #48426, #3531 ) ) ;
#61442=DIRECTION ( 'NONE',  ( 0.000000000000000000, 0.000000000000000000, -1.000000000000000000 ) ) ;
#61462=FACE_OUTER_BOUND ( 'NONE', #19554, .T. ) ;
#61482=PLANE ( 'NONE',  #77499 ) ;
#61546=VECTOR ( 'NONE', #61842, 1000.000000000000114 ) ;
#61576=AXIS2_PLACEMENT_3D ( 'NONE', #17721, #4977, #73116 ) ;
#61613=AXIS2_PLACEMENT_3D ( 'NONE', #15965, #10040, #59498 ) ;
#61646=VERTEX_POINT ( 'NONE', #71257 ) ;
#61720=ADVANCED_FACE ( 'NONE', ( #2207 ), #21422, .F. ) ;
#61731=AXIS2_PLACEMENT_3D ( 'NONE', #29793, #57488, #62955 ) ;
#61736=ORIENTED_EDGE ( 'NONE', *, *, #5250, .T. ) ;
#61759=CARTESIAN_POINT ( 'NONE',  ( 23.05014237293025658, 77.82658263289009426, 303.5238209633477595 ) ) ;
#61768=CARTESIAN_POINT ( 'NONE',  ( 38.10000000000000142, 69.84999999999999432, 358.0130000000000337 ) ) ;
#61807=EDGE_CURVE ( 'NONE', #7823, #53584, #64876, .T. ) ;
#61818=SHAPE_REPRESENTATION_RELATIONSHIP ( 'NONE' , 'NONE' ,  #28740, #44568 ) ;
#61840=DIRECTION ( 'NONE',  ( 1.000000000000000000, 0.000000000000000000, 0.000000000000000000 ) ) ;
#61842=DIRECTION ( 'NONE',  ( 0.000000000000000000, -0.5000000000000007772, 0.8660254037844381525 ) ) ;
#61843=CARTESIAN_POINT ( 'NONE',  ( 7.661254700127844153, 66.45253841614081125, 320.6630000000000109 ) ) ;
#61911=DIRECTION ( 'NONE',  ( -1.092739197465703932E-16, 0.000000000000000000, 1.000000000000000000 ) ) ;
#61967=DIRECTION ( 'NONE',  ( 0.000000000000000000, -1.000000000000000000, 0.000000000000000000 ) ) ;
#62027=EDGE_CURVE ( 'NONE', #43505, #86449, #46144, .T. ) ;
#62045=CARTESIAN_POINT ( 'NONE',  ( 69.25310000000000343, 82.54999999999999716, 335.3740053999999304 ) ) ;
#62111=ORIENTED_EDGE ( 'NONE', *, *, #11215, .T. ) ;
#62118=AXIS2_PLACEMENT_3D ( 'NONE', #62404, #182, #46183 ) ;
#62122=ORIENTED_EDGE ( 'NONE', *, *, #33739, .T. ) ;
#62125=DIRECTION ( 'NONE',  ( 0.000000000000000000, 0.000000000000000000, 1.000000000000000000 ) ) ;
#62167=DIRECTION ( 'NONE',  ( 0.000000000000000000, 0.000000000000000000, -1.000000000000000000 ) ) ;
#62244=CIRCLE ( 'NONE', #86893, 8.928100000000000591 ) ;
#62300=DIRECTION ( 'NONE',  ( 9.299908063537919123E-17, 0.000000000000000000, 1.000000000000000000 ) ) ;
#62315=CARTESIAN_POINT ( 'NONE',  ( 23.58228359103286920, 84.94115763029901700, 298.7645859682927494 ) ) ;
#62342=CARTESIAN_POINT ( 'NONE',  ( -9.493160772977415007, 90.87556570329743977, 118.1767503086004183 ) ) ;
#62350=AXIS2_PLACEMENT_3D ( 'NONE', #52342, #43319, #16093 ) ;
#62351=ORIENTED_EDGE ( 'NONE', *, *, #59193, .T. ) ;
#62365=EDGE_LOOP ( 'NONE', ( #81486, #38932 ) ) ;
#62371=EDGE_LOOP ( 'NONE', ( #54380, #89745, #17925, #15831 ) ) ;
#62404=CARTESIAN_POINT ( 'NONE',  ( 52.38749999999999574, 94.53880000000000905, 250.8250000000000171 ) ) ;
#62419=AXIS2_PLACEMENT_3D ( 'NONE', #69036, #61311, #6800 ) ;
#62475=DIRECTION ( 'NONE',  ( 0.000000000000000000, 0.000000000000000000, -1.000000000000000000 ) ) ;
#62498=CARTESIAN_POINT ( 'NONE',  ( 6.349999999999999645, 82.54999999999999716, 298.1325000000000500 ) ) ;
#62502=AXIS2_PLACEMENT_3D ( 'NONE', #10351, #32121, #65317 ) ;
#62569=VERTEX_POINT ( 'NONE', #2327 ) ;
#62573=CIRCLE ( 'NONE', #7474, 6.857999999999975671 ) ;
#62592=DIRECTION ( 'NONE',  ( 0.000000000000000000, 0.000000000000000000, -1.000000000000000000 ) ) ;
#62631=EDGE_CURVE ( 'NONE', #82352, #46935, #88344, .T. ) ;
#62646=FACE_OUTER_BOUND ( 'NONE', #72459, .T. ) ;
#62647=VECTOR ( 'NONE', #16486, 1000.000000000000000 ) ;
#62650=CARTESIAN_POINT ( 'NONE',  ( 0.000000000000000000, 67.86880000000000734, 265.5569999999999595 ) ) ;
#62670=CARTESIAN_POINT ( 'NONE',  ( 23.58223258890940954, 80.15849456350082392, 298.7647790503681335 ) ) ;
#62703=CYLINDRICAL_SURFACE ( 'NONE', #51519, 3.000000000000002665 ) ;
#62742=DIRECTION ( 'NONE',  ( 1.000000000000000000, 0.000000000000000000, 0.000000000000000000 ) ) ;
#62765=DIRECTION ( 'NONE',  ( 0.000000000000000000, 0.000000000000000000, 1.000000000000000000 ) ) ;
#62797=LINE ( 'NONE', #19687, #75871 ) ;
#62862=ORIENTED_EDGE ( 'NONE', *, *, #36466, .T. ) ;
#62869=CARTESIAN_POINT ( 'NONE',  ( 82.54999999999999716, 95.25000000000000000, 280.2255000000000109 ) ) ;
#62877=ORIENTED_EDGE ( 'NONE', *, *, #53206, .F. ) ;
#62943=ADVANCED_FACE ( 'NONE', ( #54452 ), #81143, .F. ) ;
#62944=DIRECTION ( 'NONE',  ( 0.000000000000000000, 0.000000000000000000, -1.000000000000000000 ) ) ;
#62955=DIRECTION ( 'NONE',  ( 1.000000000000000000, 0.000000000000000000, 0.000000000000000000 ) ) ;
#63014=CIRCLE ( 'NONE', #29705, 8.928100000000000591 ) ;
#63058=DIRECTION ( 'NONE',  ( -1.000000000000000000, 0.000000000000000000, -9.713237310806269221E-16 ) ) ;
#63176=VECTOR ( 'NONE', #61967, 1000.000000000000000 ) ;
#63277=UNCERTAINTY_MEASURE_WITH_UNIT (LENGTH_MEASURE( 1.000000000000000082E-05 ), #42909, 'distance_accuracy_value', 'NONE');
#63306=CONICAL_SURFACE ( 'NONE', #15474, 8.928100000000000591, 1.029744258676653645 ) ;
#63316=LINE ( 'NONE', #50569, #82062 ) ;
#63332=DIRECTION ( 'NONE',  ( 0.000000000000000000, -1.000000000000000000, 0.000000000000000000 ) ) ;
#63383=CIRCLE ( 'NONE', #8277, 3.000000000000002665 ) ;
#63441=CARTESIAN_POINT ( 'NONE',  ( 0.000000000000000000, 67.86880000000000734, 265.5569999999999595 ) ) ;
#63475=LINE ( 'NONE', #30308, #64859 ) ;
#63528=ADVANCED_FACE ( 'NONE', ( #57956 ), #86128, .T. ) ;
#63544=CARTESIAN_POINT ( 'NONE',  ( 88.90000000000000568, 66.67499999999999716, 244.4749999999999943 ) ) ;
#63566=ORIENTED_EDGE ( 'NONE', *, *, #66890, .F. ) ;
#63607=FACE_OUTER_BOUND ( 'NONE', #56956, .T. ) ;
#63682=CYLINDRICAL_SURFACE ( 'NONE', #83674, 3.968750000000020872 ) ;
#63703=DIRECTION ( 'NONE',  ( 0.4999999999999998890, 0.8660254037844387076, 0.000000000000000000 ) ) ;
#63719=B_SPLINE_CURVE_WITH_KNOTS ( 'NONE', 3,
 ( #74193, #20577, #81028, #11971, #40100, #6934, #34181, #68277, #60538, #32844, #67816, #62342, #13750, #54155, #6058, #82363, #88286, #26042, #75536, #55053, #41435, #39654, #6483, #82813, #67356 ),
 .UNSPECIFIED., .F., .F.,
 ( 4, 2, 2, 1, 2, 2, 2, 2, 2, 2, 2, 2, 4 ),
 ( 0.03942115529576777772, 0.04188556809382155272, 0.04311777449284841940, 0.04434998089187528608, 0.04558218729090215277, 0.04681439368992901945, 0.04927880648798271812, 0.05051101288700958480, 0.05174321928603645149, 0.05420763208409021261, 0.05543983848311708623, 0.05667204488214395985, 0.05913645768019770710 ),
 .UNSPECIFIED. ) ;
#63832=CARTESIAN_POINT ( 'NONE',  ( 82.54999999999999716, 69.84999999999999432, 346.0750000000000455 ) ) ;
#63903=CARTESIAN_POINT ( 'NONE',  ( 8.214917746879109858E-16, 60.82030000000000314, 272.1149787991095081 ) ) ;
#63945=CIRCLE ( 'NONE', #7395, 8.928100000000000591 ) ;
#63947=CARTESIAN_POINT ( 'NONE',  ( 3.258238535833978489, 94.72845588462597277, 118.5118799964233460 ) ) ;
#63981=ORIENTED_EDGE ( 'NONE', *, *, #12120, .F. ) ;
#63994=ORIENTED_EDGE ( 'NONE', *, *, #65049, .F. ) ;
#64016=AXIS2_PLACEMENT_3D ( 'NONE', #23411, #50634, #4619 ) ;
#64025=AXIS2_PLACEMENT_3D ( 'NONE', #22630, #57115, #29889 ) ;
#64062=DIRECTION ( 'NONE',  ( 1.000000000000000000, 0.000000000000000000, 1.986798540846734824E-16 ) ) ;
#64080=CARTESIAN_POINT ( 'NONE',  ( 60.32499999999999574, 82.54999999999999716, 358.0130000000000337 ) ) ;
#64123=CARTESIAN_POINT ( 'NONE',  ( 23.44896873141045290, 85.70058346011398953, 299.3102295797750116 ) ) ;
#64135=CARTESIAN_POINT ( 'NONE',  ( 0.000000000000000000, 50.79999999999999716, 258.6990000000000123 ) ) ;
#64165=ORIENTED_EDGE ( 'NONE', *, *, #4379, .F. ) ;
#64174=EDGE_CURVE ( 'NONE', #16125, #24379, #25732, .T. ) ;
#64183=PRODUCT_DEFINITION_CONTEXT ( 'detailed design', #1124, 'design' ) ;
#64187=DIRECTION ( 'NONE',  ( 1.000000000000000000, 0.000000000000000000, 0.000000000000000000 ) ) ;
#64225=ORIENTED_EDGE ( 'NONE', *, *, #81656, .F. ) ;
#64231=CARTESIAN_POINT ( 'NONE',  ( 85.72499999999999432, 66.67499999999999716, 346.0750000000000455 ) ) ;
#64234=VECTOR ( 'NONE', #83318, 1000.000000000000000 ) ;
#64236=CARTESIAN_POINT ( 'NONE',  ( 12.51814237086690262, 80.89737214551436750, 117.8933722897785685 ) ) ;
#64239=ORIENTED_EDGE ( 'NONE', *, *, #44765, .F. ) ;
#64253=EDGE_LOOP ( 'NONE', ( #58484, #68018, #11136 ) ) ;
#64331=FACE_OUTER_BOUND ( 'NONE', #23126, .T. ) ;
#64332=ADVANCED_FACE ( 'NONE', ( #57466 ), #7980, .T. ) ;
#64354=VECTOR ( 'NONE', #301, 1000.000000000000000 ) ;
#64393=CARTESIAN_POINT ( 'NONE',  ( 10.91394734298260794, 88.85994971916933594, 118.0527383321748118 ) ) ;
#64397=DIRECTION ( 'NONE',  ( 0.000000000000000000, 0.000000000000000000, -1.000000000000000000 ) ) ;
#64411=CARTESIAN_POINT ( 'NONE',  ( 60.32499999999999574, 82.54999999999999716, 344.4418053999999643 ) ) ;
#64430=DIRECTION ( 'NONE',  ( 1.986798540846734824E-16, 0.000000000000000000, -1.000000000000000000 ) ) ;
#64449=VERTEX_POINT ( 'NONE', #22082 ) ;
#64522=ORIENTED_EDGE ( 'NONE', *, *, #81098, .F. ) ;
#64539=DIRECTION ( 'NONE',  ( 0.000000000000000000, 0.000000000000000000, -1.000000000000000000 ) ) ;
#64552=AXIS2_PLACEMENT_3D ( 'NONE', #76465, #42817, #7871 ) ;
#64566=CARTESIAN_POINT ( 'NONE',  ( 23.62187231118733521, 84.66434562521884288, 307.1737385415713675 ) ) ;
#64584=ORIENTED_EDGE ( 'NONE', *, *, #46555, .F. ) ;
#64616=VECTOR ( 'NONE', #24113, 1000.000000000000000 ) ;
#64642=EDGE_LOOP ( 'NONE', ( #16761, #34385, #39562, #81545 ) ) ;
#64698=DIRECTION ( 'NONE',  ( 0.000000000000000000, 1.000000000000000000, 0.000000000000000000 ) ) ;
#64735=DIRECTION ( 'NONE',  ( -0.000000000000000000, -0.000000000000000000, 1.000000000000000000 ) ) ;
#64759=FACE_OUTER_BOUND ( 'NONE', #17549, .T. ) ;
#64764=EDGE_LOOP ( 'NONE', ( #55207, #80942, #73592, #79871 ) ) ;
#64799=VECTOR ( 'NONE', #26801, 1000.000000000000000 ) ;
#64836=EDGE_CURVE ( 'NONE', #4499, #52329, #38691, .T. ) ;
#64850=FACE_OUTER_BOUND ( 'NONE', #79925, .T. ) ;
#64859=VECTOR ( 'NONE', #29416, 1000.000000000000000 ) ;
#64876=LINE ( 'NONE', #2660, #78032 ) ;
#64892=EDGE_CURVE ( 'NONE', #64449, #17979, #38254, .T. ) ;
#64974=DIRECTION ( 'NONE',  ( 0.000000000000000000, 0.000000000000000000, 1.000000000000000000 ) ) ;
#64980=ADVANCED_FACE ( 'NONE', ( #31882 ), #39146, .T. ) ;
#64993=CYLINDRICAL_SURFACE ( 'NONE', #54466, 5.562600000000000655 ) ;
#65049=EDGE_CURVE ( 'NONE', #44952, #51066, #62244, .T. ) ;
#65051=ORIENTED_EDGE ( 'NONE', *, *, #84149, .T. ) ;
#65140=LINE ( 'NONE', #2923, #76660 ) ;
#65203=CARTESIAN_POINT ( 'NONE',  ( -44.45000000000000284, 50.79999999999999716, 275.4630000000000223 ) ) ;
#65209=CIRCLE ( 'NONE', #47800, 16.09746158385918946 ) ;
#65225=VERTEX_POINT ( 'NONE', #14594 ) ;
#65232=LINE ( 'NONE', #45642, #80844 ) ;
#65256=DIRECTION ( 'NONE',  ( 0.000000000000000000, 0.000000000000000000, -1.000000000000000000 ) ) ;
#65293=DIRECTION ( 'NONE',  ( 0.000000000000000000, -1.000000000000000000, 0.000000000000000000 ) ) ;
#65317=DIRECTION ( 'NONE',  ( 0.000000000000000000, 0.000000000000000000, 1.000000000000000000 ) ) ;
#65323=LINE ( 'NONE', #37624, #36628 ) ;
#65329=ORIENTED_EDGE ( 'NONE', *, *, #42602, .T. ) ;
#65337=DIRECTION ( 'NONE',  ( -0.000000000000000000, -0.000000000000000000, -1.000000000000000000 ) ) ;
#65355=AXIS2_PLACEMENT_3D ( 'NONE', #78191, #31345, #59037 ) ;
#65364=LINE ( 'NONE', #11281, #51215 ) ;
#65388=EDGE_LOOP ( 'NONE', ( #38422, #68068, #37999, #28200 ) ) ;
#65405=VERTEX_POINT ( 'NONE', #9568 ) ;
#65428=AXIS2_PLACEMENT_3D ( 'NONE', #82567, #8031, #21216 ) ;
#65438=CARTESIAN_POINT ( 'NONE',  ( 6.938893903907229955E-15, 50.79999999999999716, 216.0269999999999868 ) ) ;
#65439=VERTEX_POINT ( 'NONE', #33907 ) ;
#65443=LINE ( 'NONE', #79090, #70323 ) ;
#65454=CARTESIAN_POINT ( 'NONE',  ( 23.49602257209429723, 85.45800003945487333, 306.6792945138783466 ) ) ;
#65508=CARTESIAN_POINT ( 'NONE',  ( -0.4111448617337906675, 69.95000000000001705, 118.5560000000000258 ) ) ;
#65591=ADVANCED_FACE ( 'NONE', ( #55662 ), #18943, .T. ) ;
#65637=CARTESIAN_POINT ( 'NONE',  ( 52.99265158129170317, 95.25000000000000000, 358.0130000000000337 ) ) ;
#65687=DIRECTION ( 'NONE',  ( 1.000000000000000000, 0.000000000000000000, 0.000000000000000000 ) ) ;
#65693=ORIENTED_EDGE ( 'NONE', *, *, #85284, .T. ) ;
#65694=EDGE_CURVE ( 'NONE', #75348, #45281, #22537, .T. ) ;
#65705=DIRECTION ( 'NONE',  ( -1.000000000000000000, 0.000000000000000000, 0.000000000000000000 ) ) ;
#65771=ORIENTED_EDGE ( 'NONE', *, *, #49594, .T. ) ;
#65833=ORIENTED_EDGE ( 'NONE', *, *, #80588, .F. ) ;
#65849=FACE_OUTER_BOUND ( 'NONE', #32252, .T. ) ;
#65863=VECTOR ( 'NONE', #79154, 1000.000000000000000 ) ;
#65878=ORIENTED_EDGE ( 'NONE', *, *, #56675, .T. ) ;
#65936=EDGE_CURVE ( 'NONE', #31578, #1197, #5662, .T. ) ;
#65998=CARTESIAN_POINT ( 'NONE',  ( 57.14999999999999858, 95.25000000000000000, 326.2630000000000337 ) ) ;
#66024=EDGE_CURVE ( 'NONE', #31809, #46288, #36253, .T. ) ;
#66081=ORIENTED_EDGE ( 'NONE', *, *, #22960, .F. ) ;
#66122=CARTESIAN_POINT ( 'NONE',  ( 44.45000000000000284, 114.2999999999999972, 275.4630000000000223 ) ) ;
#66197=ORIENTED_EDGE ( 'NONE', *, *, #9742, .T. ) ;
#66272=DIRECTION ( 'NONE',  ( 0.000000000000000000, 1.000000000000000000, 0.000000000000000000 ) ) ;
#66375=DIRECTION ( 'NONE',  ( 0.000000000000000000, 0.000000000000000000, 1.000000000000000000 ) ) ;
#66387=CARTESIAN_POINT ( 'NONE',  ( -3.273551063997644839, 70.35480798052911666, 118.5135525315334633 ) ) ;
#66434=VERTEX_POINT ( 'NONE', #87322 ) ;
#66440=DIRECTION ( 'NONE',  ( -1.000000000000000000, 0.000000000000000000, 0.000000000000000000 ) ) ;
#66497=VECTOR ( 'NONE', #33370, 1000.000000000000000 ) ;
#66562=EDGE_LOOP ( 'NONE', ( #32857, #78616, #75091, #11058, #41516 ) ) ;
#66598=CARTESIAN_POINT ( 'NONE',  ( -7.661254700127833495, 95.64746158385918307, 320.6630000000000109 ) ) ;
#66636=AXIS2_PLACEMENT_3D ( 'NONE', #13842, #41524, #15188 ) ;
#66661=ADVANCED_FACE ( 'NONE', ( #49094 ), #83649, .T. ) ;
#66683=DIRECTION ( 'NONE',  ( 0.000000000000000000, 0.000000000000000000, 1.000000000000000000 ) ) ;
#66730=ORIENTED_EDGE ( 'NONE', *, *, #27922, .T. ) ;
#66754=VERTEX_POINT ( 'NONE', #20960 ) ;
#66758=CARTESIAN_POINT ( 'NONE',  ( 44.45000000000000284, 111.1250000000000000, 257.1750000000000114 ) ) ;
#66763=EDGE_LOOP ( 'NONE', ( #44130, #64225 ) ) ;
#66772=DIRECTION ( 'NONE',  ( 1.000000000000000000, 0.000000000000000000, -9.299908063537909262E-17 ) ) ;
#66784=LINE ( 'NONE', #61308, #30122 ) ;
#66788=CARTESIAN_POINT ( 'NONE',  ( 60.32499999999999574, 82.54999999999999716, 344.4418053999999643 ) ) ;
#66798=CARTESIAN_POINT ( 'NONE',  ( 23.18019461599323350, 78.27143315885348329, 300.7803427218691468 ) ) ;
#66890=EDGE_CURVE ( 'NONE', #47202, #70326, #85004, .T. ) ;
#66897=ADVANCED_FACE ( 'NONE', ( #3646 ), #72626, .F. ) ;
#66917=EDGE_CURVE ( 'NONE', #79853, #68630, #26195, .T. ) ;
#66952=AXIS2_PLACEMENT_3D ( 'NONE', #46831, #4629, #60011 ) ;
#66997=ORIENTED_EDGE ( 'NONE', *, *, #76159, .F. ) ;
#67025=EDGE_LOOP ( 'NONE', ( #68352, #46632 ) ) ;
#67041=VECTOR ( 'NONE', #30754, 999.9999999999998863 ) ;
#67060=VERTEX_POINT ( 'NONE', #70348 ) ;
#67077=DIRECTION ( 'NONE',  ( -1.821231995776179916E-16, 0.000000000000000000, -1.000000000000000000 ) ) ;
#67117=DIRECTION ( 'NONE',  ( 0.000000000000000000, 0.000000000000000000, 1.000000000000000000 ) ) ;
#67120=ORIENTED_EDGE ( 'NONE', *, *, #71459, .T. ) ;
#67125=LINE ( 'NONE', #80329, #87086 ) ;
#67150=CARTESIAN_POINT ( 'NONE',  ( 31.75000000000000000, 69.84999999999999432, 342.8999999999999773 ) ) ;
#67163=CARTESIAN_POINT ( 'NONE',  ( 45.66030316258350297, 82.54999999999999716, 358.0130000000000337 ) ) ;
#67217=ADVANCED_FACE ( 'NONE', ( #42616, #22211 ), #54893, .F. ) ;
#67243=FACE_OUTER_BOUND ( 'NONE', #35882, .T. ) ;
#67265=CARTESIAN_POINT ( 'NONE',  ( 7.661254700127833495, 82.54999999999999716, 320.6630000000000109 ) ) ;
#67266=EDGE_CURVE ( 'NONE', #31158, #66754, #65323, .T. ) ;
#67294=CARTESIAN_POINT ( 'NONE',  ( 60.32499999999999574, 82.54999999999999716, 344.4418053999999643 ) ) ;
#67308=FACE_OUTER_BOUND ( 'NONE', #86917, .T. ) ;
#67309=AXIS2_PLACEMENT_3D ( 'NONE', #55491, #116, #75972 ) ;
#67346=CARTESIAN_POINT ( 'NONE',  ( 7.778756678762479992E-15, 50.79999999999999716, 222.8849999999999909 ) ) ;
#67356=CARTESIAN_POINT ( 'NONE',  ( 0.000000000000000000, 95.14999999999999147, 118.5560000000000116 ) ) ;
#67372=ORIENTED_EDGE ( 'NONE', *, *, #51323, .T. ) ;
#67478=MECHANICAL_DESIGN_GEOMETRIC_PRESENTATION_REPRESENTATION('',(#60199),#18146);
#67496=ORIENTED_EDGE ( 'NONE', *, *, #65694, .F. ) ;
#67500=CYLINDRICAL_SURFACE ( 'NONE', #35950, 16.09746158385918946 ) ;
#67519=DIRECTION ( 'NONE',  ( 0.8571673007021118895, 0.000000000000000000, 0.5150380749100549327 ) ) ;
#67533=DIRECTION ( 'NONE',  ( 0.000000000000000000, 0.000000000000000000, -1.000000000000000000 ) ) ;
#67566=DIRECTION ( 'NONE',  ( 1.000000000000000000, 0.000000000000000000, 0.000000000000000000 ) ) ;
#67579=AXIS2_PLACEMENT_3D ( 'NONE', #21902, #42753, #41415 ) ;
#67587=ORIENTED_EDGE ( 'NONE', *, *, #55807, .F. ) ;
#67616=LINE ( 'NONE', #26718, #38791 ) ;
#67666=VECTOR ( 'NONE', #39669, 1000.000000000000000 ) ;
#67702=VECTOR ( 'NONE', #24926, 1000.000000000000000 ) ;
#67748=FACE_BOUND ( 'NONE', #4072, .T. ) ;
#67764=AXIS2_PLACEMENT_3D ( 'NONE', #55660, #34348, #82981 ) ;
#67765=AXIS2_PLACEMENT_3D ( 'NONE', #39518, #25441, #53108 ) ;
#67784=CIRCLE ( 'NONE', #41708, 6.857999999999975671 ) ;
#67806=DIRECTION ( 'NONE',  ( 1.000000000000000000, 0.000000000000000000, -9.299908063537909262E-17 ) ) ;
#67815=ORIENTED_EDGE ( 'NONE', *, *, #53872, .T. ) ;
#67816=CARTESIAN_POINT ( 'NONE',  ( -10.01454657728489472, 90.24125983913356208, 118.1331779202407262 ) ) ;
#67824=AXIS2_PLACEMENT_3D ( 'NONE', #59998, #66375, #53169 ) ;
#67837=AXIS2_PLACEMENT_3D ( 'NONE', #44781, #37540, #80221 ) ;
#67901=LINE ( 'NONE', #6571, #69411 ) ;
#67934=VECTOR ( 'NONE', #2994, 1000.000000000000000 ) ;
#67955=ORIENTED_EDGE ( 'NONE', *, *, #47071, .T. ) ;
#68001=CARTESIAN_POINT ( 'NONE',  ( 34.92499999999999716, 87.13271776169258942, 310.8325000000000387 ) ) ;
#68018=ORIENTED_EDGE ( 'NONE', *, *, #70932, .T. ) ;
#68035=ORIENTED_EDGE ( 'NONE', *, *, #62027, .F. ) ;
#68068=ORIENTED_EDGE ( 'NONE', *, *, #7761, .F. ) ;
#68083=CARTESIAN_POINT ( 'NONE',  ( 88.90000000000000568, 69.84999999999999432, 346.0750000000000455 ) ) ;
#68092=UNCERTAINTY_MEASURE_WITH_UNIT (LENGTH_MEASURE( 1.000000000000000082E-05 ), #72782, 'distance_accuracy_value', 'NONE');
#68133=LINE ( 'NONE', #19528, #29927 ) ;
#68167=ORIENTED_EDGE ( 'NONE', *, *, #21849, .T. ) ;
#68209=SURFACE_STYLE_USAGE ( .BOTH. , #60016 ) ;
#68277=CARTESIAN_POINT ( 'NONE',  ( -11.30816021491739853, 88.12274986616640149, 118.0156291604116205 ) ) ;
#68285=DIRECTION ( 'NONE',  ( 0.000000000000000000, -1.000000000000000000, 0.000000000000000000 ) ) ;
#68352=ORIENTED_EDGE ( 'NONE', *, *, #53550, .T. ) ;
#68371=ORIENTED_EDGE ( 'NONE', *, *, #61295, .T. ) ;
#68387=EDGE_CURVE ( 'NONE', #32579, #18726, #59727, .T. ) ;
#68391=LINE ( 'NONE', #52910, #83521 ) ;
#68410=VERTEX_POINT ( 'NONE', #57955 ) ;
#68506=CARTESIAN_POINT ( 'NONE',  ( 52.38749999999999574, 94.53880000000000905, 225.4249999999999829 ) ) ;
#68546=ORIENTED_EDGE ( 'NONE', *, *, #44096, .T. ) ;
#68550=EDGE_CURVE ( 'NONE', #77621, #86161, #67901, .T. ) ;
#68569=CARTESIAN_POINT ( 'NONE',  ( -7.661254700127833495, 82.54999999999999716, 317.6630000000000109 ) ) ;
#68571=EDGE_CURVE ( 'NONE', #14287, #68627, #42861, .T. ) ;
#68578=EDGE_CURVE ( 'NONE', #50184, #74884, #77407, .T. ) ;
#68611=AXIS2_PLACEMENT_3D ( 'NONE', #3186, #77803, #15580 ) ;
#68627=VERTEX_POINT ( 'NONE', #62869 ) ;
#68630=VERTEX_POINT ( 'NONE', #36071 ) ;
#68675=ORIENTED_EDGE ( 'NONE', *, *, #76567, .F. ) ;
#68742=DIRECTION ( 'NONE',  ( 1.000000000000000000, 0.000000000000000000, 0.000000000000000000 ) ) ;
#68764=CARTESIAN_POINT ( 'NONE',  ( 82.54999999999999716, 95.25000000000000000, 358.0130000000000337 ) ) ;
#68782=ADVANCED_FACE ( 'NONE', ( #51899 ), #10153, .T. ) ;
#68799=AXIS2_PLACEMENT_3D ( 'NONE', #57037, #295, #21194 ) ;
#68821=TOROIDAL_SURFACE ( 'NONE', #45566, 13.09746158385919124, 3.000000000000000000 ) ;
#68887=FACE_OUTER_BOUND ( 'NONE', #19844, .T. ) ;
#68900=CARTESIAN_POINT ( 'NONE',  ( 85.72499999999999432, 69.84999999999999432, 346.0750000000000455 ) ) ;
#68975=LINE ( 'NONE', #6742, #71237 ) ;
#69036=CARTESIAN_POINT ( 'NONE',  ( 0.000000000000000000, 67.86880000000000734, 265.5569999999999595 ) ) ;
#69038=ORIENTED_EDGE ( 'NONE', *, *, #5392, .F. ) ;
#69077=CARTESIAN_POINT ( 'NONE',  ( 28.57499999999999929, 82.54999999999999716, 298.1325000000000500 ) ) ;
#69152=FACE_OUTER_BOUND ( 'NONE', #56661, .T. ) ;
#69206=CARTESIAN_POINT ( 'NONE',  ( 12.59999999999999964, 82.54999999999999716, -190.5010000000000048 ) ) ;
#69272=DIRECTION ( 'NONE',  ( -0.02992792722492259097, 3.665114028111639174E-18, 0.9995520592605567911 ) ) ;
#69411=VECTOR ( 'NONE', #81114, 1000.000000000000000 ) ;
#69417=CARTESIAN_POINT ( 'NONE',  ( 5.586628598344671737, 93.87391117675657881, 118.4267587378186306 ) ) ;
#69421=LINE ( 'NONE', #47158, #20051 ) ;
#69434=CARTESIAN_POINT ( 'NONE',  ( 44.45000000000000284, 66.67499999999999716, 219.0749999999999886 ) ) ;
#69436=ORIENTED_EDGE ( 'NONE', *, *, #71459, .F. ) ;
#69441=FACE_OUTER_BOUND ( 'NONE', #74434, .T. ) ;
#69453=DIRECTION ( 'NONE',  ( 1.049727191138617833E-16, -0.5150380749100549327, 0.8571673007021118895 ) ) ;
#69484=VECTOR ( 'NONE', #74890, 1000.000000000000000 ) ;
#69487=CARTESIAN_POINT ( 'NONE',  ( 69.25310000000000343, 82.54999999999999716, 358.0130000000000337 ) ) ;
#69509=VERTEX_POINT ( 'NONE', #15313 ) ;
#69514=CARTESIAN_POINT ( 'NONE',  ( -44.45000000000000284, 114.2999999999999972, 275.4630000000000223 ) ) ;
#69536=PLANE ( 'NONE',  #74191 ) ;
#69553=ADVANCED_FACE ( 'NONE', ( #17095 ), #73833, .F. ) ;
#69595=CARTESIAN_POINT ( 'NONE',  ( 82.54999999999999716, 69.84999999999999432, 280.2255000000000109 ) ) ;
#69614=VECTOR ( 'NONE', #51526, 1000.000000000000000 ) ;
#69615=ADVANCED_FACE ( 'NONE', ( #44327 ), #45216, .T. ) ;
#69623=VERTEX_POINT ( 'NONE', #4355 ) ;
#69696=VERTEX_POINT ( 'NONE', #26577 ) ;
#69720=CIRCLE ( 'NONE', #45047, 3.174999999999983391 ) ;
#69724=ORIENTED_EDGE ( 'NONE', *, *, #62631, .F. ) ;
#69764=CYLINDRICAL_SURFACE ( 'NONE', #80433, 12.59999999999999964 ) ;
#69802=EDGE_CURVE ( 'NONE', #49324, #39002, #15649, .T. ) ;
#69815=FACE_OUTER_BOUND ( 'NONE', #85394, .T. ) ;
#69843=VERTEX_POINT ( 'NONE', #35627 ) ;
#69853=DIRECTION ( 'NONE',  ( 1.000000000000000000, -0.000000000000000000, -0.000000000000000000 ) ) ;
#69864=CARTESIAN_POINT ( 'NONE',  ( 2.859107348890838729, 94.82819007650195431, 118.5222036340525591 ) ) ;
#69925=VECTOR ( 'NONE', #58863, 1000.000000000000000 ) ;
#69985=LINE ( 'NONE', #70893, #48033 ) ;
#70013=DIRECTION ( 'NONE',  ( 0.000000000000000000, 1.000000000000000000, 0.000000000000000000 ) ) ;
#70042=DIRECTION ( 'NONE',  ( 1.000000000000000000, 0.000000000000000000, 0.000000000000000000 ) ) ;
#70065=DIRECTION ( 'NONE',  ( 0.000000000000000000, -1.000000000000000000, 0.000000000000000000 ) ) ;
#70068=VERTEX_POINT ( 'NONE', #31379 ) ;
#70117=VECTOR ( 'NONE', #44067, 1000.000000000000000 ) ;
#70141=FACE_OUTER_BOUND ( 'NONE', #1930, .T. ) ;
#70167=VERTEX_POINT ( 'NONE', #52246 ) ;
#70215=CARTESIAN_POINT ( 'NONE',  ( 7.661254700127844153, 69.45253841614081125, 320.6630000000000109 ) ) ;
#70218=ADVANCED_FACE ( 'NONE', ( #67243 ), #53132, .F. ) ;
#70235=VERTEX_POINT ( 'NONE', #82247 ) ;
#70239=ORIENTED_EDGE ( 'NONE', *, *, #68387, .F. ) ;
#70304=EDGE_CURVE ( 'NONE', #56973, #70579, #16854, .T. ) ;
#70305=AXIS2_PLACEMENT_3D ( 'NONE', #30066, #8739, #14651 ) ;
#70308=CARTESIAN_POINT ( 'NONE',  ( 11.30280982162985026, 88.13356536631488325, 118.0161419656921140 ) ) ;
#70310=CARTESIAN_POINT ( 'NONE',  ( 20.75871628398702384, 82.54999999999999716, 317.6630000000000109 ) ) ;
#70323=VECTOR ( 'NONE', #10916, 1000.000000000000000 ) ;
#70326=VERTEX_POINT ( 'NONE', #15437 ) ;
#70342=ORIENTED_EDGE ( 'NONE', *, *, #31975, .T. ) ;
#70346=CARTESIAN_POINT ( 'NONE',  ( 6.938893903907229955E-15, 60.82030000000000314, 216.0269999999999868 ) ) ;
#70348=CARTESIAN_POINT ( 'NONE',  ( 28.57499999999999929, 73.38456447661469895, 302.8950000000000387 ) ) ;
#70363=DIRECTION ( 'NONE',  ( 0.000000000000000000, 1.000000000000000000, 0.000000000000000000 ) ) ;
#70381=CARTESIAN_POINT ( 'NONE',  ( 6.938893903907229955E-15, 67.86880000000000734, 210.4643999999999835 ) ) ;
#70385=VERTEX_POINT ( 'NONE', #35855 ) ;
#70390=CARTESIAN_POINT ( 'NONE',  ( 23.71377214814948076, 81.30938561711869283, 298.2863242343943284 ) ) ;
#70427=LINE ( 'NONE', #9538, #28066 ) ;
#70457=ORIENTED_EDGE ( 'NONE', *, *, #50333, .F. ) ;
#70477=DIRECTION ( 'NONE',  ( 0.000000000000000000, -0.4999999999999998890, -0.8660254037844387076 ) ) ;
#70551=FACE_OUTER_BOUND ( 'NONE', #46825, .T. ) ;
#70553=PLANE ( 'NONE',  #16989 ) ;
#70579=VERTEX_POINT ( 'NONE', #58529 ) ;
#70618=EDGE_CURVE ( 'NONE', #17829, #70235, #3575, .T. ) ;
#70661=DIRECTION ( 'NONE',  ( 0.000000000000000000, -1.000000000000000000, 0.000000000000000000 ) ) ;
#70771=CARTESIAN_POINT ( 'NONE',  ( 6.938893903907229955E-15, 50.79999999999999716, 216.0269999999999868 ) ) ;
#70790=VECTOR ( 'NONE', #44543, 1000.000000000000000 ) ;
#70824=ADVANCED_FACE ( 'NONE', ( #50609, #41995 ), #36096, .F. ) ;
#70828=EDGE_LOOP ( 'NONE', ( #34752, #31066, #49785, #17902, #13940, #67120 ) ) ;
#70835=EDGE_CURVE ( 'NONE', #86595, #77621, #57425, .T. ) ;
#70862=LINE ( 'NONE', #79012, #80208 ) ;
#70880=ORIENTED_EDGE ( 'NONE', *, *, #19345, .F. ) ;
#70881=AXIS2_PLACEMENT_3D ( 'NONE', #53041, #59438, #86722 ) ;
#70893=CARTESIAN_POINT ( 'NONE',  ( 82.54999999999999716, 69.84999999999999432, 280.2255000000000109 ) ) ;
#70899=DIRECTION ( 'NONE',  ( 0.000000000000000000, 0.000000000000000000, 1.000000000000000000 ) ) ;
#70905=ORIENTED_EDGE ( 'NONE', *, *, #81339, .F. ) ;
#70915=DIRECTION ( 'NONE',  ( -0.7071067811865475727, 0.000000000000000000, 0.7071067811865475727 ) ) ;
#70932=EDGE_CURVE ( 'NONE', #73971, #42802, #65140, .T. ) ;
#70981=EDGE_CURVE ( 'NONE', #69843, #70068, #63719, .T. ) ;
#70994=VERTEX_POINT ( 'NONE', #5147 ) ;
#71058=DIRECTION ( 'NONE',  ( -1.784063995862374817E-16, 0.000000000000000000, -1.000000000000000000 ) ) ;
#71065=CARTESIAN_POINT ( 'NONE',  ( 10.24823761126901722, 75.20812216786193005, 118.1124527501650618 ) ) ;
#71068=EDGE_LOOP ( 'NONE', ( #19348, #38160, #33958, #75132 ) ) ;
#71080=ORIENTED_EDGE ( 'NONE', *, *, #49594, .F. ) ;
#71100=VERTEX_POINT ( 'NONE', #49595 ) ;
#71222=DIRECTION ( 'NONE',  ( 0.000000000000000000, -1.000000000000000000, 0.000000000000000000 ) ) ;
#71234=CARTESIAN_POINT ( 'NONE',  ( 34.92499999999999716, 77.96728223830740490, 310.8325000000000387 ) ) ;
#71236=ORIENTED_EDGE ( 'NONE', *, *, #2732, .F. ) ;
#71237=VECTOR ( 'NONE', #34441, 1000.000000000000000 ) ;
#71253=VECTOR ( 'NONE', #20962, 1000.000000000000000 ) ;
#71257=CARTESIAN_POINT ( 'NONE',  ( 44.45000000000000284, 69.84999999999999432, 257.1750000000000114 ) ) ;
#71321=ORIENTED_EDGE ( 'NONE', *, *, #87449, .T. ) ;
#71381=CARTESIAN_POINT ( 'NONE',  ( 45.66030316258350297, 82.54999999999999716, 346.9005000000000223 ) ) ;
#71395=CARTESIAN_POINT ( 'NONE',  ( 23.18025296944486868, 86.82834877582368449, 300.7800082948225509 ) ) ;
#71404=ORIENTED_EDGE ( 'NONE', *, *, #65694, .T. ) ;
#71426=DIRECTION ( 'NONE',  ( 0.000000000000000000, 0.000000000000000000, -1.000000000000000000 ) ) ;
#71434=ORIENTED_EDGE ( 'NONE', *, *, #77772, .F. ) ;
#71459=EDGE_CURVE ( 'NONE', #84598, #69696, #21363, .T. ) ;
#71537=CARTESIAN_POINT ( 'NONE',  ( 34.92499999999999716, 73.38456447661469895, 302.8950000000000387 ) ) ;
#71569=CARTESIAN_POINT ( 'NONE',  ( 0.000000000000000000, 50.79999999999999716, 265.5569999999999595 ) ) ;
#71686=CARTESIAN_POINT ( 'NONE',  ( -7.661254700127833495, 69.45253841614081125, 320.6630000000000109 ) ) ;
#71693=AXIS2_PLACEMENT_3D ( 'NONE', #27084, #5753, #41141 ) ;
#71811=CARTESIAN_POINT ( 'NONE',  ( 60.32499999999999574, 82.54999999999999716, 344.4418053999999643 ) ) ;
#71830=CARTESIAN_POINT ( 'NONE',  ( 23.11215236101587323, 87.06814822297243950, 304.4331722187091032 ) ) ;
#71884=ADVANCED_FACE ( 'NONE', ( #50615 ), #78798, .F. ) ;
#71948=CARTESIAN_POINT ( 'NONE',  ( 3.266167974950230146, 70.37369935891477724, 118.5116585762504684 ) ) ;
#71980=ORIENTED_EDGE ( 'NONE', *, *, #39427, .T. ) ;
#72003=B_SPLINE_CURVE_WITH_KNOTS ( 'NONE', 3,
 ( #28508, #818, #56202, #69864, #63947, #7634, #57106, #69417, #29880, #84852, #49845, #36693, #367, #22619, #35775, #50755, #64393, #70308, #22177, #50294, #57562, #83953, #34882, #21264, #21724 ),
 .UNSPECIFIED., .F., .F.,
 ( 4, 2, 2, 2, 2, 2, 2, 2, 2, 1, 2, 2, 4 ),
 ( 0.05913645768019770710, 0.06159852758862928435, 0.06282956254284507991, 0.06406059749706087547, 0.06652266740549245272, 0.06775370235970824828, 0.06898473731392402997, 0.07144680722235557946, 0.07267784217657137502, 0.07390887713078717058, 0.07513991208500296615, 0.07637094703921876171, 0.07883301694765033896 ),
 .UNSPECIFIED. ) ;
#72042=ORIENTED_EDGE ( 'NONE', *, *, #31975, .F. ) ;
#72073=ORIENTED_EDGE ( 'NONE', *, *, #46201, .T. ) ;
#72111=FACE_OUTER_BOUND ( 'NONE', #16711, .T. ) ;
#72279=CARTESIAN_POINT ( 'NONE',  ( 23.11423962701955759, 87.05952208832691497, 301.3555005791828307 ) ) ;
#72303=ORIENTED_EDGE ( 'NONE', *, *, #45198, .F. ) ;
#72326=AXIS2_PLACEMENT_3D ( 'NONE', #1589, #57876, #64698 ) ;
#72393=CARTESIAN_POINT ( 'NONE',  ( 52.38749999999999574, 94.53880000000000905, 246.8562499999999886 ) ) ;
#72394=CARTESIAN_POINT ( 'NONE',  ( 10.00076313689444696, 74.87425971760926302, 118.1337365946718876 ) ) ;
#72395=EDGE_CURVE ( 'NONE', #10129, #17742, #33342, .T. ) ;
#72422=ORIENTED_EDGE ( 'NONE', *, *, #36171, .T. ) ;
#72446=EDGE_CURVE ( 'NONE', #34033, #59761, #9192, .T. ) ;
#72459=EDGE_LOOP ( 'NONE', ( #78300, #89549 ) ) ;
#72460=EDGE_CURVE ( 'NONE', #46472, #69509, #47847, .T. ) ;
#72508=FACE_OUTER_BOUND ( 'NONE', #53243, .T. ) ;
#72524=CARTESIAN_POINT ( 'NONE',  ( 67.65734841870819594, 95.25000000000000000, 346.9005000000000223 ) ) ;
#72529=ORIENTED_EDGE ( 'NONE', *, *, #75533, .F. ) ;
#72583=EDGE_CURVE ( 'NONE', #61646, #82905, #46353, .T. ) ;
#72626=CONICAL_SURFACE ( 'NONE', #65355, 5.562600000000000655, 1.029744258676653645 ) ;
#72669=CARTESIAN_POINT ( 'NONE',  ( 69.25310000000000343, 82.54999999999999716, 335.3740053999999304 ) ) ;
#72671=PLANE ( 'NONE',  #72874 ) ;
#72672=VECTOR ( 'NONE', #54552, 1000.000000000000000 ) ;
#72687=VECTOR ( 'NONE', #7292, 1000.000000000000000 ) ;
#72699=AXIS2_PLACEMENT_3D ( 'NONE', #8489, #35274, #7588 ) ;
#72712=DIRECTION ( 'NONE',  ( 0.000000000000000000, 0.000000000000000000, -1.000000000000000000 ) ) ;
#72720=CARTESIAN_POINT ( 'NONE',  ( 23.74045948899717473, 83.33176929200182315, 307.5955140303815369 ) ) ;
#72782=( LENGTH_UNIT ( ) NAMED_UNIT ( * ) SI_UNIT ( .MILLI., .METRE. ) );
#72853=VECTOR ( 'NONE', #50219, 999.9999999999998863 ) ;
#72874=AXIS2_PLACEMENT_3D ( 'NONE', #56435, #15121, #84628 ) ;
#72892=CARTESIAN_POINT ( 'NONE',  ( 45.66030316258350297, 82.54999999999999716, 346.9005000000000223 ) ) ;
#72911=ORIENTED_EDGE ( 'NONE', *, *, #23651, .F. ) ;
#72930=ORIENTED_EDGE ( 'NONE', *, *, #27074, .F. ) ;
#72947=VERTEX_POINT ( 'NONE', #29528 ) ;
#72956=ORIENTED_EDGE ( 'NONE', *, *, #77502, .F. ) ;
#73039=AXIS2_PLACEMENT_3D ( 'NONE', #54375, #82144, #19442 ) ;
#73084=DIRECTION ( 'NONE',  ( 0.4999999999999998890, -0.8660254037844387076, 0.000000000000000000 ) ) ;
#73116=DIRECTION ( 'NONE',  ( 0.000000000000000000, 0.000000000000000000, -1.000000000000000000 ) ) ;
#73216=FACE_OUTER_BOUND ( 'NONE', #40767, .T. ) ;
#73280=ORIENTED_EDGE ( 'NONE', *, *, #10308, .T. ) ;
#73298=DIRECTION ( 'NONE',  ( 1.000000000000000000, 0.000000000000000000, 0.000000000000000000 ) ) ;
#73387=DIRECTION ( 'NONE',  ( 1.000000000000000000, 0.000000000000000000, 0.000000000000000000 ) ) ;
#73431=CARTESIAN_POINT ( 'NONE',  ( 63.50000000000000000, 66.67499999999999716, 219.0749999999999886 ) ) ;
#73461=EDGE_CURVE ( 'NONE', #8926, #31809, #10305, .T. ) ;
#73525=EDGE_LOOP ( 'NONE', ( #63994, #54651 ) ) ;
#73552=ORIENTED_EDGE ( 'NONE', *, *, #89069, .T. ) ;
#73577=DIRECTION ( 'NONE',  ( 0.000000000000000000, 0.000000000000000000, 1.000000000000000000 ) ) ;
#73592=ORIENTED_EDGE ( 'NONE', *, *, #57401, .T. ) ;
#73599=LINE ( 'NONE', #82233, #80687 ) ;
#73602=CARTESIAN_POINT ( 'NONE',  ( -44.45000000000000284, 114.2999999999999972, 206.3750000000000000 ) ) ;
#73615=CARTESIAN_POINT ( 'NONE',  ( 23.05726497218590154, 77.84977045057786427, 303.6782364904642009 ) ) ;
#73646=PLANE ( 'NONE',  #67824 ) ;
#73703=LINE ( 'NONE', #74593, #61546 ) ;
#73779=EDGE_CURVE ( 'NONE', #32950, #41217, #62573, .T. ) ;
#73798=LINE ( 'NONE', #65203, #36364 ) ;
#73801=AXIS2_PLACEMENT_3D ( 'NONE', #2807, #85494, #84595 ) ;
#73815=AXIS2_PLACEMENT_3D ( 'NONE', #25741, #62944, #50206 ) ;
#73833=PLANE ( 'NONE',  #67837 ) ;
#73847=AXIS2_PLACEMENT_3D ( 'NONE', #26424, #5993, #26862 ) ;
#73855=EDGE_CURVE ( 'NONE', #71100, #1395, #49537, .T. ) ;
#73939=CARTESIAN_POINT ( 'NONE',  ( 34.92499999999999716, 77.96728223830740490, 310.8325000000000387 ) ) ;
#73971=VERTEX_POINT ( 'NONE', #13230 ) ;
#74017=DIRECTION ( 'NONE',  ( 1.000000000000000000, -0.000000000000000000, -0.000000000000000000 ) ) ;
#74022=VERTEX_POINT ( 'NONE', #27295 ) ;
#74039=FACE_OUTER_BOUND ( 'NONE', #62371, .T. ) ;
#74047=VECTOR ( 'NONE', #6861, 1000.000000000000000 ) ;
#74059=EDGE_LOOP ( 'NONE', ( #17627, #27568 ) ) ;
#74061=CARTESIAN_POINT ( 'NONE',  ( 28.57499999999999929, 77.96728223830740490, 310.8325000000000387 ) ) ;
#74074=ADVANCED_FACE ( 'NONE', ( #34553, #20935, #76344 ), #69536, .F. ) ;
#74085=CARTESIAN_POINT ( 'NONE',  ( 44.45000000000000284, 66.67499999999999716, 257.1750000000000114 ) ) ;
#74093=EDGE_CURVE ( 'NONE', #80239, #34761, #69985, .T. ) ;
#74099=CARTESIAN_POINT ( 'NONE',  ( 67.65734841870819594, 69.84999999999999432, 346.9005000000000223 ) ) ;
#74114=PLANE ( 'NONE',  #86523 ) ;
#74118=CYLINDRICAL_SURFACE ( 'NONE', #66952, 16.09746158385918946 ) ;
#74122=FILL_AREA_STYLE_COLOUR ( '', #52120 ) ;
#74132=CIRCLE ( 'NONE', #82840, 5.562600000000000655 ) ;
#74175=ORIENTED_EDGE ( 'NONE', *, *, #74964, .T. ) ;
#74191=AXIS2_PLACEMENT_3D ( 'NONE', #489, #28180, #55870 ) ;
#74192=ADVANCED_FACE ( 'NONE', ( #4063 ), #79046, .F. ) ;
#74193=CARTESIAN_POINT ( 'NONE',  ( -12.59999999999999964, 82.54999999999999716, 117.8845415480757595 ) ) ;
#74194=DIRECTION ( 'NONE',  ( 1.000000000000000000, 0.000000000000000000, 0.000000000000000000 ) ) ;
#74222=VERTEX_POINT ( 'NONE', #72669 ) ;
#74297=ORIENTED_EDGE ( 'NONE', *, *, #59139, .F. ) ;
#74349=LINE ( 'NONE', #19382, #23076 ) ;
#74434=EDGE_LOOP ( 'NONE', ( #13578, #54834, #21498 ) ) ;
#74497=VECTOR ( 'NONE', #79283, 1000.000000000000000 ) ;
#74514=DIRECTION ( 'NONE',  ( 0.000000000000000000, 0.000000000000000000, -1.000000000000000000 ) ) ;
#74564=CIRCLE ( 'NONE', #26699, 3.968749999999992895 ) ;
#74593=CARTESIAN_POINT ( 'NONE',  ( 34.92499999999999716, 77.96728223830730542, 294.9574999999999818 ) ) ;
#74689=CARTESIAN_POINT ( 'NONE',  ( 28.57499999999999929, 87.13271776169258942, 310.8325000000000387 ) ) ;
#74739=PLANE ( 'NONE',  #57654 ) ;
#74741=ORIENTED_EDGE ( 'NONE', *, *, #62631, .T. ) ;
#74756=VECTOR ( 'NONE', #12457, 1000.000000000000000 ) ;
#74793=DIRECTION ( 'NONE',  ( 0.000000000000000000, 1.000000000000000000, 0.000000000000000000 ) ) ;
#74884=VERTEX_POINT ( 'NONE', #81627 ) ;
#74886=DIRECTION ( 'NONE',  ( 0.000000000000000000, 0.000000000000000000, -1.000000000000000000 ) ) ;
#74890=DIRECTION ( 'NONE',  ( -0.4999999999999998890, 0.8660254037844387076, 0.000000000000000000 ) ) ;
#74906=EDGE_LOOP ( 'NONE', ( #66997, #80436, #4902, #2127 ) ) ;
#74964=EDGE_CURVE ( 'NONE', #51227, #70326, #20640, .T. ) ;
#74968=VERTEX_POINT ( 'NONE', #33891 ) ;
#75007=DIRECTION ( 'NONE',  ( -1.000000000000000000, 0.000000000000000000, 1.821231995776179916E-16 ) ) ;
#75008=DIRECTION ( 'NONE',  ( 1.000000000000000000, 0.000000000000000000, 0.000000000000000000 ) ) ;
#75019=ORIENTED_EDGE ( 'NONE', *, *, #66024, .T. ) ;
#75022=EDGE_CURVE ( 'NONE', #23386, #28274, #32538, .T. ) ;
#75033=LINE ( 'NONE', #32334, #6016 ) ;
#75034=VECTOR ( 'NONE', #8687, 1000.000000000000000 ) ;
#75035=AXIS2_PLACEMENT_3D ( 'NONE', #188, #15167, #21996 ) ;
#75077=DIRECTION ( 'NONE',  ( -1.000000000000000000, 0.000000000000000000, 0.000000000000000000 ) ) ;
#75091=ORIENTED_EDGE ( 'NONE', *, *, #38001, .F. ) ;
#75119=EDGE_CURVE ( 'NONE', #31809, #9455, #42396, .T. ) ;
#75132=ORIENTED_EDGE ( 'NONE', *, *, #20417, .T. ) ;
#75185=AXIS2_PLACEMENT_3D ( 'NONE', #59015, #87199, #31771 ) ;
#75307=CARTESIAN_POINT ( 'NONE',  ( -44.45000000000000284, 50.79999999999999716, 257.1750000000000114 ) ) ;
#75348=VERTEX_POINT ( 'NONE', #38359 ) ;
#75418=CARTESIAN_POINT ( 'NONE',  ( 23.75871628398702384, 82.54999999999999716, 307.6575000000000273 ) ) ;
#75436=CYLINDRICAL_SURFACE ( 'NONE', #16694, 3.968749999999992895 ) ;
#75489=CARTESIAN_POINT ( 'NONE',  ( 28.57499999999999929, 87.13271776169258942, 310.8325000000000387 ) ) ;
#75517=AXIS2_PLACEMENT_3D ( 'NONE', #75489, #13260, #40946 ) ;
#75533=EDGE_CURVE ( 'NONE', #67060, #37287, #88326, .T. ) ;
#75536=CARTESIAN_POINT ( 'NONE',  ( -4.446177000103011423, 94.34669717174053005, 118.4732138684817215 ) ) ;
#75609=ORIENTED_EDGE ( 'NONE', *, *, #19345, .T. ) ;
#75618=ORIENTED_EDGE ( 'NONE', *, *, #53482, .T. ) ;
#75644=EDGE_LOOP ( 'NONE', ( #56342, #23340, #66081, #45485 ) ) ;
#75698=VERTEX_POINT ( 'NONE', #7425 ) ;
#75704=DIRECTION ( 'NONE',  ( 1.000000000000000000, 0.000000000000000000, -9.299908063537909262E-17 ) ) ;
#75706=CARTESIAN_POINT ( 'NONE',  ( 23.75871628398702384, 82.54999999999999716, 307.6575000000000273 ) ) ;
#75708=CARTESIAN_POINT ( 'NONE',  ( 44.45000000000000284, 50.79999999999999716, 275.4630000000000223 ) ) ;
#75721=VERTEX_POINT ( 'NONE', #21517 ) ;
#75737=VERTEX_POINT ( 'NONE', #84199 ) ;
#75740=DIRECTION ( 'NONE',  ( 0.000000000000000000, 0.000000000000000000, 1.000000000000000000 ) ) ;
#75784=DIRECTION ( 'NONE',  ( 0.000000000000000000, -1.000000000000000000, 0.000000000000000000 ) ) ;
#75818=DIRECTION ( 'NONE',  ( 1.000000000000000000, 0.000000000000000000, 0.000000000000000000 ) ) ;
#75850=DIRECTION ( 'NONE',  ( 0.000000000000000000, 0.000000000000000000, 1.000000000000000000 ) ) ;
#75866=ORIENTED_EDGE ( 'NONE', *, *, #79068, .F. ) ;
#75871=VECTOR ( 'NONE', #20592, 1000.000000000000000 ) ;
#75877=FACE_OUTER_BOUND ( 'NONE', #49102, .T. ) ;
#75933=VERTEX_POINT ( 'NONE', #59576 ) ;
#75951=EDGE_CURVE ( 'NONE', #34761, #15433, #65364, .T. ) ;
#75956=CARTESIAN_POINT ( 'NONE',  ( 23.74939270293513616, 83.17752536574882072, 298.1637491577495780 ) ) ;
#75972=DIRECTION ( 'NONE',  ( 1.000000000000000000, 0.000000000000000000, 0.000000000000000000 ) ) ;
#76064=DIRECTION ( 'NONE',  ( 9.299908063537919123E-17, 0.000000000000000000, 1.000000000000000000 ) ) ;
#76066=EDGE_LOOP ( 'NONE', ( #74297, #25145, #74175, #63566, #71321, #40262 ) ) ;
#76159=EDGE_CURVE ( 'NONE', #65225, #81285, #35188, .T. ) ;
#76239=CIRCLE ( 'NONE', #16789, 3.174999999999983391 ) ;
#76251=CARTESIAN_POINT ( 'NONE',  ( 52.38749999999999574, 94.53880000000000905, 225.4249999999999829 ) ) ;
#76286=ORIENTED_EDGE ( 'NONE', *, *, #42615, .T. ) ;
#76329=VERTEX_POINT ( 'NONE', #39003 ) ;
#76344=FACE_BOUND ( 'NONE', #66763, .T. ) ;
#76350=EDGE_CURVE ( 'NONE', #34574, #53327, #81594, .T. ) ;
#76430=EDGE_LOOP ( 'NONE', ( #53068, #3507, #44906, #67372 ) ) ;
#76457=ORIENTED_EDGE ( 'NONE', *, *, #55731, .F. ) ;
#76465=CARTESIAN_POINT ( 'NONE',  ( 7.661254700127833495, 82.54999999999999716, 275.4630000000000223 ) ) ;
#76503=ORIENTED_EDGE ( 'NONE', *, *, #53550, .F. ) ;
#76567=EDGE_CURVE ( 'NONE', #86245, #52932, #28503, .T. ) ;
#76585=ORIENTED_EDGE ( 'NONE', *, *, #29017, .F. ) ;
#76587=LINE ( 'NONE', #62498, #79061 ) ;
#76617=EDGE_CURVE ( 'NONE', #1814, #79502, #8078, .T. ) ;
#76620=ORIENTED_EDGE ( 'NONE', *, *, #86499, .T. ) ;
#76660=VECTOR ( 'NONE', #86935, 999.9999999999998863 ) ;
#76667=LINE ( 'NONE', #14450, #30038 ) ;
#76675=VECTOR ( 'NONE', #21281, 1000.000000000000000 ) ;
#76766=LINE ( 'NONE', #37109, #12446 ) ;
#76771=LINE ( 'NONE', #14558, #5079 ) ;
#76780=VECTOR ( 'NONE', #77051, 1000.000000000000000 ) ;
#76786=DIRECTION ( 'NONE',  ( 0.000000000000000000, 0.000000000000000000, -1.000000000000000000 ) ) ;
#76788=CARTESIAN_POINT ( 'NONE',  ( 7.661254700127833495, 69.45253841614081125, 317.6630000000000109 ) ) ;
#76864=DIRECTION ( 'NONE',  ( 1.000000000000000000, 0.000000000000000000, -9.299908063537909262E-17 ) ) ;
#76873=DIRECTION ( 'NONE',  ( -1.000000000000000000, 0.000000000000000000, -1.748382715945130038E-14 ) ) ;
#76884=CARTESIAN_POINT ( 'NONE',  ( 67.65734841870819594, 69.84999999999999432, 346.9005000000000223 ) ) ;
#76923=VECTOR ( 'NONE', #63703, 1000.000000000000000 ) ;
#76925=PRODUCT_DEFINITION_FORMATION_WITH_SPECIFIED_SOURCE ( 'ANY', '', #1904, .NOT_KNOWN. ) ;
#76938=LINE ( 'NONE', #28790, #58139 ) ;
#76989=ORIENTED_EDGE ( 'NONE', *, *, #87449, .F. ) ;
#77017=CARTESIAN_POINT ( 'NONE',  ( 0.000000000000000000, 50.79999999999999716, 265.5569999999999595 ) ) ;
#77034=LINE ( 'NONE', #77473, #7876 ) ;
#77051=DIRECTION ( 'NONE',  ( 1.000000000000000000, 0.000000000000000000, 0.000000000000000000 ) ) ;
#77085=EDGE_CURVE ( 'NONE', #70326, #66434, #60566, .T. ) ;
#77088=DIRECTION ( 'NONE',  ( -1.000000000000000000, 0.000000000000000000, 0.000000000000000000 ) ) ;
#77097=CYLINDRICAL_SURFACE ( 'NONE', #86208, 3.174999999999983391 ) ;
#77116=ORIENTED_EDGE ( 'NONE', *, *, #73461, .F. ) ;
#77136=DIRECTION ( 'NONE',  ( 0.000000000000000000, 0.000000000000000000, 1.000000000000000000 ) ) ;
#77147=VERTEX_POINT ( 'NONE', #11994 ) ;
#77151=DIRECTION ( 'NONE',  ( 1.000000000000000000, 0.000000000000000000, 0.000000000000000000 ) ) ;
#77211=CARTESIAN_POINT ( 'NONE',  ( 23.74939251434799203, 81.92209703240837371, 298.1637470768533831 ) ) ;
#77219=CARTESIAN_POINT ( 'NONE',  ( 57.14999999999999858, 60.86974387893089755, 329.4379999999999882 ) ) ;
#77263=EDGE_CURVE ( 'NONE', #9455, #53584, #59228, .T. ) ;
#77266=CARTESIAN_POINT ( 'NONE',  ( 47.62500000000000000, 66.67499999999999716, 292.1000000000000227 ) ) ;
#77288=DIRECTION ( 'NONE',  ( 0.4999999999999998890, -0.8660254037844387076, 0.000000000000000000 ) ) ;
#77298=DIRECTION ( 'NONE',  ( -1.000000000000000000, 0.000000000000000000, 1.821231995776179916E-16 ) ) ;
#77329=CARTESIAN_POINT ( 'NONE',  ( 0.000000000000000000, 60.82030000000000314, 265.5569999999999595 ) ) ;
#77333=ORIENTED_EDGE ( 'NONE', *, *, #26510, .F. ) ;
#77344=LINE ( 'NONE', #38141, #6237 ) ;
#77405=DIRECTION ( 'NONE',  ( -1.092739197465703932E-16, 1.000000000000000000, 0.000000000000000000 ) ) ;
#77407=LINE ( 'NONE', #7913, #21570 ) ;
#77408=CARTESIAN_POINT ( 'NONE',  ( 38.10000000000000142, 95.25000000000000000, 346.9005000000000223 ) ) ;
#77419=ADVANCED_FACE ( 'NONE', ( #61462 ), #55076, .F. ) ;
#77463=VERTEX_POINT ( 'NONE', #56886 ) ;
#77466=EDGE_CURVE ( 'NONE', #30868, #54369, #44942, .T. ) ;
#77473=CARTESIAN_POINT ( 'NONE',  ( 47.62500000000000000, 69.84999999999999432, 257.1750000000000114 ) ) ;
#77496=ADVANCED_FACE ( 'NONE', ( #31765 ), #72671, .F. ) ;
#77499=AXIS2_PLACEMENT_3D ( 'NONE', #68764, #55995, #41926 ) ;
#77501=CIRCLE ( 'NONE', #22382, 3.174999999999983391 ) ;
#77502=EDGE_CURVE ( 'NONE', #79692, #50744, #77344, .T. ) ;
#77503=ORIENTED_EDGE ( 'NONE', *, *, #38089, .F. ) ;
#77508=CARTESIAN_POINT ( 'NONE',  ( 34.92499999999999716, 82.54999999999999716, 315.3410000000000082 ) ) ;
#77525=CYLINDRICAL_SURFACE ( 'NONE', #72699, 12.44600000000001216 ) ;
#77532=ADVANCED_FACE ( 'NONE', ( #84178 ), #18135, .F. ) ;
#77605=AXIS2_PLACEMENT_3D ( 'NONE', #155, #55085, #82848 ) ;
#77621=VERTEX_POINT ( 'NONE', #87635 ) ;
#77638=VECTOR ( 'NONE', #3773, 1000.000000000000114 ) ;
#77710=DIRECTION ( 'NONE',  ( -0.000000000000000000, 1.000000000000000000, 0.000000000000000000 ) ) ;
#77743=CARTESIAN_POINT ( 'NONE',  ( 38.10000000000000142, 95.25000000000000000, 346.9005000000000223 ) ) ;
#77772=EDGE_CURVE ( 'NONE', #80239, #84598, #32657, .T. ) ;
#77782=FACE_OUTER_BOUND ( 'NONE', #21793, .T. ) ;
#77786=ORIENTED_EDGE ( 'NONE', *, *, #27173, .T. ) ;
#77802=EDGE_CURVE ( 'NONE', #12424, #86245, #34445, .T. ) ;
#77803=DIRECTION ( 'NONE',  ( -1.000000000000000000, 0.000000000000000000, 1.784063995862374817E-16 ) ) ;
#77862=FACE_BOUND ( 'NONE', #45325, .T. ) ;
#77875=DIRECTION ( 'NONE',  ( 0.000000000000000000, -1.000000000000000000, 0.000000000000000000 ) ) ;
#77911=FILL_AREA_STYLE ('',( #55627 ) ) ;
#77984=ORIENTED_EDGE ( 'NONE', *, *, #12162, .T. ) ;
#77996=ORIENTED_EDGE ( 'NONE', *, *, #70981, .F. ) ;
#78001=ORIENTED_EDGE ( 'NONE', *, *, #16409, .F. ) ;
#78032=VECTOR ( 'NONE', #9915, 1000.000000000000000 ) ;
#78039=CARTESIAN_POINT ( 'NONE',  ( 60.32499999999999574, 82.54999999999999716, 335.3740053999999304 ) ) ;
#78063=CARTESIAN_POINT ( 'NONE',  ( 7.620115932400929327E-15, 67.86880000000000734, 221.5895999999999901 ) ) ;
#78069=ORIENTED_EDGE ( 'NONE', *, *, #82638, .F. ) ;
#78083=ORIENTED_EDGE ( 'NONE', *, *, #66917, .T. ) ;
#78137=DIRECTION ( 'NONE',  ( 9.299908063537919123E-17, 0.000000000000000000, 1.000000000000000000 ) ) ;
#78191=CARTESIAN_POINT ( 'NONE',  ( 6.938893903907229955E-15, 67.86880000000000734, 216.0269999999999868 ) ) ;
#78205=FACE_OUTER_BOUND ( 'NONE', #78611, .T. ) ;
#78215=EDGE_CURVE ( 'NONE', #46288, #78417, #54758, .T. ) ;
#78265=DIRECTION ( 'NONE',  ( 0.000000000000000000, 0.000000000000000000, -1.000000000000000000 ) ) ;
#78267=EDGE_LOOP ( 'NONE', ( #43094, #30787 ) ) ;
#78274=CARTESIAN_POINT ( 'NONE',  ( 63.50000000000000000, 69.84999999999999432, 219.0749999999999886 ) ) ;
#78278=FACE_BOUND ( 'NONE', #73525, .T. ) ;
#78300=ORIENTED_EDGE ( 'NONE', *, *, #10249, .T. ) ;
#78358=DIRECTION ( 'NONE',  ( 0.000000000000000000, -1.000000000000000000, 0.000000000000000000 ) ) ;
#78386=CARTESIAN_POINT ( 'NONE',  ( 34.92499999999999716, 66.67499999999999716, 295.2750000000000341 ) ) ;
#78417=VERTEX_POINT ( 'NONE', #70215 ) ;
#78464=DIRECTION ( 'NONE',  ( 0.000000000000000000, -0.4999999999999998890, -0.8660254037844387076 ) ) ;
#78501=VECTOR ( 'NONE', #65705, 1000.000000000000000 ) ;
#78503=DIRECTION ( 'NONE',  ( 1.000000000000000000, 0.000000000000000000, 0.000000000000000000 ) ) ;
#78516=EDGE_CURVE ( 'NONE', #28761, #89263, #78835, .T. ) ;
#78572=CARTESIAN_POINT ( 'NONE',  ( 6.812220284937080487E-16, 67.86880000000000734, 271.1195999999999913 ) ) ;
#78601=CARTESIAN_POINT ( 'NONE',  ( -7.661254700127833495, 66.45253841614081125, 317.6630000000000109 ) ) ;
#78603=CARTESIAN_POINT ( 'NONE',  ( 70.99299999999999500, 82.54999999999999716, 358.0130000000000337 ) ) ;
#78611=EDGE_LOOP ( 'NONE', ( #2937, #21387, #66730, #42316, #29738, #21745, #65771, #41165, #65878, #7222, #2216, #50071, #13414 ) ) ;
#78616=ORIENTED_EDGE ( 'NONE', *, *, #56331, .F. ) ;
#78667=CARTESIAN_POINT ( 'NONE',  ( 47.62500000000000000, 69.84999999999999432, 260.3500000000000227 ) ) ;
#78669=CARTESIAN_POINT ( 'NONE',  ( 23.68747463269394160, 84.09014500043505791, 307.4123016622365299 ) ) ;
#78761=ADVANCED_FACE ( 'NONE', ( #605, #28774 ), #61482, .F. ) ;
#78798=PLANE ( 'NONE',  #47781 ) ;
#78835=LINE ( 'NONE', #9332, #74497 ) ;
#78863=ORIENTED_EDGE ( 'NONE', *, *, #45260, .T. ) ;
#78905=CARTESIAN_POINT ( 'NONE',  ( 57.14999999999999858, 69.84999999999999432, 297.6879999999999882 ) ) ;
#78909=ORIENTED_EDGE ( 'NONE', *, *, #79559, .F. ) ;
#78925=VECTOR ( 'NONE', #45493, 1000.000000000000000 ) ;
#78956=VECTOR ( 'NONE', #87078, 1000.000000000000000 ) ;
#78984=FACE_OUTER_BOUND ( 'NONE', #89387, .T. ) ;
#79012=CARTESIAN_POINT ( 'NONE',  ( 0.000000000000000000, 50.79999999999999716, 259.9944000000000415 ) ) ;
#79046=CYLINDRICAL_SURFACE ( 'NONE', #50968, 3.174999999999983391 ) ;
#79050=ADVANCED_FACE ( 'NONE', ( #73216 ), #59577, .F. ) ;
#79061=VECTOR ( 'NONE', #41590, 1000.000000000000000 ) ;
#79064=CYLINDRICAL_SURFACE ( 'NONE', #31115, 3.174999999999983391 ) ;
#79068=EDGE_CURVE ( 'NONE', #29470, #80239, #87757, .T. ) ;
#79086=AXIS2_PLACEMENT_3D ( 'NONE', #63441, #49799, #16202 ) ;
#79090=CARTESIAN_POINT ( 'NONE',  ( -44.45000000000000284, 114.2999999999999972, 257.1750000000000114 ) ) ;
#79129=CARTESIAN_POINT ( 'NONE',  ( -44.45000000000000284, 114.2999999999999972, 206.3750000000000000 ) ) ;
#79154=DIRECTION ( 'NONE',  ( 0.000000000000000000, 0.4999999999999998890, 0.8660254037844387076 ) ) ;
#79165=ORIENTED_EDGE ( 'NONE', *, *, #48328, .F. ) ;
#79235=ORIENTED_EDGE ( 'NONE', *, *, #12162, .F. ) ;
#79249=ORIENTED_EDGE ( 'NONE', *, *, #14313, .T. ) ;
#79254=ADVANCED_FACE ( 'NONE', ( #85450 ), #79064, .F. ) ;
#79271=CONICAL_SURFACE ( 'NONE', #28476, 5.562600000000000655, 1.029744258676653645 ) ;
#79283=DIRECTION ( 'NONE',  ( -0.4999999999999998890, -0.8660254037844387076, 0.000000000000000000 ) ) ;
#79288=ORIENTED_EDGE ( 'NONE', *, *, #73855, .F. ) ;
#79340=ADVANCED_FACE ( 'NONE', ( #46287 ), #87212, .F. ) ;
#79367=DIRECTION ( 'NONE',  ( 0.000000000000000000, 1.000000000000000000, 0.000000000000000000 ) ) ;
#79388=ORIENTED_EDGE ( 'NONE', *, *, #5250, .F. ) ;
#79399=CONICAL_SURFACE ( 'NONE', #67765, 5.562599999999973122, 1.029744258676653645 ) ;
#79484=CIRCLE ( 'NONE', #35955, 3.000000000000002665 ) ;
#79485=LINE ( 'NONE', #67163, #9697 ) ;
#79502=VERTEX_POINT ( 'NONE', #49771 ) ;
#79515=DIRECTION ( 'NONE',  ( 1.000000000000000000, 0.000000000000000000, 0.000000000000000000 ) ) ;
#79532=LINE ( 'NONE', #85012, #64616 ) ;
#79543=CIRCLE ( 'NONE', #75185, 3.174999999999983391 ) ;
#79549=CARTESIAN_POINT ( 'NONE',  ( 23.04787079752263068, 87.28121659793244191, 303.5230764621404660 ) ) ;
#79559=EDGE_CURVE ( 'NONE', #50079, #74968, #57170, .T. ) ;
#79599=ORIENTED_EDGE ( 'NONE', *, *, #49028, .F. ) ;
#79680=VERTEX_POINT ( 'NONE', #16175 ) ;
#79692=VERTEX_POINT ( 'NONE', #16614 ) ;
#79749=CIRCLE ( 'NONE', #33299, 3.968749999999992895 ) ;
#79751=ADVANCED_FACE ( 'NONE', ( #64759 ), #31116, .T. ) ;
#79795=FACE_OUTER_BOUND ( 'NONE', #27509, .T. ) ;
#79820=CARTESIAN_POINT ( 'NONE',  ( 57.14999999999999858, 60.86974387893089755, 300.8629999999999995 ) ) ;
#79853=VERTEX_POINT ( 'NONE', #28318 ) ;
#79871=ORIENTED_EDGE ( 'NONE', *, *, #72460, .T. ) ;
#79925=EDGE_LOOP ( 'NONE', ( #73552, #3489, #26832, #37843, #23177 ) ) ;
#79934=DIRECTION ( 'NONE',  ( 0.000000000000000000, 0.000000000000000000, -1.000000000000000000 ) ) ;
#79936=AXIS2_PLACEMENT_3D ( 'NONE', #55060, #68285, #61442 ) ;
#79970=CARTESIAN_POINT ( 'NONE',  ( 47.62500000000000000, 111.1250000000000000, 219.0749999999999886 ) ) ;
#79972=DIRECTION ( 'NONE',  ( 0.000000000000000000, 0.000000000000000000, -1.000000000000000000 ) ) ;
#79996=CARTESIAN_POINT ( 'NONE',  ( 23.75871628398702384, 82.54999999999999716, 307.6575000000000273 ) ) ;
#80056=DIRECTION ( 'NONE',  ( -1.821231995776179916E-16, 0.000000000000000000, -1.000000000000000000 ) ) ;
#80066=DIRECTION ( 'NONE',  ( -1.092739197465703932E-16, 0.000000000000000000, 1.000000000000000000 ) ) ;
#80149=CARTESIAN_POINT ( 'NONE',  ( -7.661254700127832606, 98.64746158385918307, 320.6630000000000109 ) ) ;
#80163=LINE ( 'NONE', #11560, #69614 ) ;
#80190=ORIENTED_EDGE ( 'NONE', *, *, #17993, .F. ) ;
#80208=VECTOR ( 'NONE', #57197, 1000.000000000000000 ) ;
#80219=ORIENTED_EDGE ( 'NONE', *, *, #86004, .F. ) ;
#80221=DIRECTION ( 'NONE',  ( 0.000000000000000000, 0.000000000000000000, -1.000000000000000000 ) ) ;
#80239=VERTEX_POINT ( 'NONE', #63832 ) ;
#80246=MANIFOLD_SOLID_BREP ( 'Stock-BR-Y-104-1', #40159 ) ;
#80279=DIRECTION ( 'NONE',  ( 0.000000000000000000, 0.000000000000000000, -1.000000000000000000 ) ) ;
#80288=EDGE_LOOP ( 'NONE', ( #20600, #17258, #4859 ) ) ;
#80308=CARTESIAN_POINT ( 'NONE',  ( 28.57499999999999929, 82.54999999999999716, 302.8950000000000387 ) ) ;
#80309=ADVANCED_FACE ( 'NONE', ( #11424 ), #88196, .T. ) ;
#80329=CARTESIAN_POINT ( 'NONE',  ( 67.65734841870819594, 69.84999999999999432, 358.0130000000000337 ) ) ;
#80366=CARTESIAN_POINT ( 'NONE',  ( 28.57499999999999929, 77.96728223830740490, 310.8325000000000387 ) ) ;
#80426=ORIENTED_EDGE ( 'NONE', *, *, #56319, .F. ) ;
#80433=AXIS2_PLACEMENT_3D ( 'NONE', #37029, #64735, #43378 ) ;
#80436=ORIENTED_EDGE ( 'NONE', *, *, #20016, .F. ) ;
#80454=ORIENTED_EDGE ( 'NONE', *, *, #25990, .F. ) ;
#80479=ADVANCED_FACE ( 'NONE', ( #482 ), #62703, .T. ) ;
#80588=EDGE_CURVE ( 'NONE', #46935, #41326, #57220, .T. ) ;
#80631=VECTOR ( 'NONE', #77298, 1000.000000000000000 ) ;
#80639=CARTESIAN_POINT ( 'NONE',  ( 34.92499999999999716, 69.84999999999999432, 292.1000000000000227 ) ) ;
#80649=ORIENTED_EDGE ( 'NONE', *, *, #64174, .F. ) ;
#80651=ADVANCED_FACE ( 'NONE', ( #63607 ), #36351, .F. ) ;
#80687=VECTOR ( 'NONE', #12729, 1000.000000000000000 ) ;
#80714=LINE ( 'NONE', #73431, #28962 ) ;
#80844=VECTOR ( 'NONE', #60176, 1000.000000000000000 ) ;
#80860=CARTESIAN_POINT ( 'NONE',  ( 57.14999999999999858, 69.84999999999999432, 326.2630000000000337 ) ) ;
#80871=EDGE_CURVE ( 'NONE', #89072, #1768, #54720, .T. ) ;
#80888=VECTOR ( 'NONE', #69272, 1000.000000000000227 ) ;
#80899=VERTEX_POINT ( 'NONE', #47156 ) ;
#80929=DIRECTION ( 'NONE',  ( 0.000000000000000000, 0.000000000000000000, -1.000000000000000000 ) ) ;
#80938=DIRECTION ( 'NONE',  ( 1.561055996379579722E-16, -1.000000000000000000, 0.000000000000000000 ) ) ;
#80942=ORIENTED_EDGE ( 'NONE', *, *, #49709, .F. ) ;
#80950=CARTESIAN_POINT ( 'NONE',  ( -5.203389996554649066, 71.06717806059110387, 118.4423725322968011 ) ) ;
#80963=DIRECTION ( 'NONE',  ( 4.649954031768951549E-17, -0.8660254037844387076, 0.4999999999999998890 ) ) ;
#80989=CARTESIAN_POINT ( 'NONE',  ( -7.661254700127832606, 98.64746158385918307, 317.6630000000000109 ) ) ;
#81028=CARTESIAN_POINT ( 'NONE',  ( -12.52017803906219129, 84.19101337647619232, 117.8931578309348964 ) ) ;
#81060=ORIENTED_EDGE ( 'NONE', *, *, #23659, .T. ) ;
#81067=DIRECTION ( 'NONE',  ( 0.000000000000000000, 1.000000000000000000, 0.000000000000000000 ) ) ;
#81098=EDGE_CURVE ( 'NONE', #11575, #75698, #25763, .T. ) ;
#81114=DIRECTION ( 'NONE',  ( 1.000000000000000000, 0.000000000000000000, -9.299908063537909262E-17 ) ) ;
#81127=CARTESIAN_POINT ( 'NONE',  ( 57.14999999999999858, 95.25000000000000000, 280.2255000000000109 ) ) ;
#81135=ORIENTED_EDGE ( 'NONE', *, *, #50376, .T. ) ;
#81143=CONICAL_SURFACE ( 'NONE', #37630, 6.858000000000003205, 0.02993239667170383839 ) ;
#81191=CARTESIAN_POINT ( 'NONE',  ( 53.97500000000000142, 95.25000000000000000, 283.4005000000000223 ) ) ;
#81214=AXIS2_PLACEMENT_3D ( 'NONE', #53260, #40557, #74194 ) ;
#81285=VERTEX_POINT ( 'NONE', #39360 ) ;
#81287=ORIENTED_EDGE ( 'NONE', *, *, #24893, .F. ) ;
#81324=CARTESIAN_POINT ( 'NONE',  ( 6.938893903907229955E-15, 50.79999999999999716, 216.0269999999999868 ) ) ;
#81327=ORIENTED_EDGE ( 'NONE', *, *, #34321, .F. ) ;
#81339=EDGE_CURVE ( 'NONE', #66434, #77147, #21056, .T. ) ;
#81367=ORIENTED_EDGE ( 'NONE', *, *, #35609, .T. ) ;
#81396=DIRECTION ( 'NONE',  ( 0.000000000000000000, 0.000000000000000000, -1.000000000000000000 ) ) ;
#81406=CARTESIAN_POINT ( 'NONE',  ( -12.59999999999999964, 82.54999999999999716, 117.8845415480757595 ) ) ;
#81466=CARTESIAN_POINT ( 'NONE',  ( 28.57499999999999929, 87.13271776169258942, 310.8325000000000387 ) ) ;
#81477=PLANE ( 'NONE',  #28104 ) ;
#81486=ORIENTED_EDGE ( 'NONE', *, *, #799, .F. ) ;
#81501=DIRECTION ( 'NONE',  ( 0.000000000000000000, -1.000000000000000000, 0.000000000000000000 ) ) ;
#81545=ORIENTED_EDGE ( 'NONE', *, *, #61807, .T. ) ;
#81594=CIRCLE ( 'NONE', #29325, 3.968749999999992895 ) ;
#81627=CARTESIAN_POINT ( 'NONE',  ( -44.45000000000000284, 50.79999999999999716, 206.3750000000000000 ) ) ;
#81629=ORIENTED_EDGE ( 'NONE', *, *, #25990, .T. ) ;
#81656=EDGE_CURVE ( 'NONE', #53327, #34574, #52897, .T. ) ;
#81669=DIRECTION ( 'NONE',  ( 0.000000000000000000, 0.000000000000000000, -1.000000000000000000 ) ) ;
#81715=EDGE_LOOP ( 'NONE', ( #69038, #43229 ) ) ;
#81734=PLANE ( 'NONE',  #26153 ) ;
#81792=CARTESIAN_POINT ( 'NONE',  ( 23.18076855059904418, 78.27346916906378738, 305.0143276166587043 ) ) ;
#81817=DIRECTION ( 'NONE',  ( -0.000000000000000000, -0.000000000000000000, -1.000000000000000000 ) ) ;
#81827=FACE_OUTER_BOUND ( 'NONE', #18235, .T. ) ;
#81842=CARTESIAN_POINT ( 'NONE',  ( -11.30434772722943926, 76.96944167614310572, 118.0159957117157745 ) ) ;
#81900=ADVANCED_FACE ( 'NONE', ( #70551 ), #41390, .F. ) ;
#81911=CIRCLE ( 'NONE', #39790, 12.59999999999999964 ) ;
#81924=DIRECTION ( 'NONE',  ( -4.649954031768947235E-17, 0.8660254037844387076, -0.4999999999999998890 ) ) ;
#81936=CIRCLE ( 'NONE', #64552, 16.09746158385918946 ) ;
#82031=EDGE_LOOP ( 'NONE', ( #64239, #67815, #84734, #50058 ) ) ;
#82062=VECTOR ( 'NONE', #30140, 1000.000000000000000 ) ;
#82094=CARTESIAN_POINT ( 'NONE',  ( 34.92499999999999716, 87.13271776169270311, 294.9574999999999818 ) ) ;
#82127=CIRCLE ( 'NONE', #21228, 3.174999999999983391 ) ;
#82144=DIRECTION ( 'NONE',  ( 0.000000000000000000, -1.000000000000000000, 0.000000000000000000 ) ) ;
#82166=ORIENTED_EDGE ( 'NONE', *, *, #79559, .T. ) ;
#82180=ORIENTED_EDGE ( 'NONE', *, *, #38089, .T. ) ;
#82187=ORIENTED_EDGE ( 'NONE', *, *, #22868, .F. ) ;
#82233=CARTESIAN_POINT ( 'NONE',  ( 50.79999999999999716, 69.84999999999999432, 257.1750000000000114 ) ) ;
#82247=CARTESIAN_POINT ( 'NONE',  ( 67.65734841870819594, 69.84999999999999432, 358.0130000000000337 ) ) ;
#82291=ORIENTED_EDGE ( 'NONE', *, *, #85284, .F. ) ;
#82352=VERTEX_POINT ( 'NONE', #37830 ) ;
#82363=CARTESIAN_POINT ( 'NONE',  ( -7.341132454938143148, 92.79876842313133523, 118.3289926826412710 ) ) ;
#82423=CARTESIAN_POINT ( 'NONE',  ( 70.99299999999999500, 82.54999999999999716, 358.0130000000000337 ) ) ;
#82431=ADVANCED_FACE ( 'NONE', ( #60477 ), #52301, .F. ) ;
#82540=LINE ( 'NONE', #47968, #8366 ) ;
#82567=CARTESIAN_POINT ( 'NONE',  ( 7.661254700127822836, 98.64746158385918307, 320.6630000000000109 ) ) ;
#82638=EDGE_CURVE ( 'NONE', #75737, #21876, #24104, .T. ) ;
#82643=CYLINDRICAL_SURFACE ( 'NONE', #27107, 118.5560000000000116 ) ;
#82658=CARTESIAN_POINT ( 'NONE',  ( 5.562599999999999767, 60.82030000000000314, 216.0269999999999868 ) ) ;
#82712=FACE_OUTER_BOUND ( 'NONE', #12711, .T. ) ;
#82746=CARTESIAN_POINT ( 'NONE',  ( -12.43699715260042993, 80.48827657640002542, 117.9018778621280887 ) ) ;
#82805=CARTESIAN_POINT ( 'NONE',  ( 38.10000000000000142, 95.25000000000000000, 358.0130000000000337 ) ) ;
#82813=CARTESIAN_POINT ( 'NONE',  ( -0.8330786292759821965, 95.14999999999997726, 118.5559999999999974 ) ) ;
#82839=DIRECTION ( 'NONE',  ( 0.000000000000000000, 0.000000000000000000, 1.000000000000000000 ) ) ;
#82840=AXIS2_PLACEMENT_3D ( 'NONE', #44382, #3505, #80279 ) ;
#82841=EDGE_CURVE ( 'NONE', #7668, #32579, #41451, .T. ) ;
#82848=DIRECTION ( 'NONE',  ( 0.000000000000000000, 0.000000000000000000, 1.000000000000000000 ) ) ;
#82905=VERTEX_POINT ( 'NONE', #66758 ) ;
#82959=CARTESIAN_POINT ( 'NONE',  ( 38.10000000000000142, 69.84999999999999432, 283.4005000000000223 ) ) ;
#82968=CYLINDRICAL_SURFACE ( 'NONE', #39858, 5.562599999999973122 ) ;
#82981=DIRECTION ( 'NONE',  ( 0.000000000000000000, 0.000000000000000000, -1.000000000000000000 ) ) ;
#83026=ORIENTED_EDGE ( 'NONE', *, *, #11762, .T. ) ;
#83104=ORIENTED_EDGE ( 'NONE', *, *, #42102, .F. ) ;
#83157=PLANE ( 'NONE',  #41371 ) ;
#83208=VECTOR ( 'NONE', #57676, 1000.000000000000000 ) ;
#83215=CARTESIAN_POINT ( 'NONE',  ( 34.92499999999999716, 91.71543552338529537, 302.8950000000000387 ) ) ;
#83245=CARTESIAN_POINT ( 'NONE',  ( -7.661254700127832606, 95.64746158385918307, 320.6630000000000109 ) ) ;
#83264=CARTESIAN_POINT ( 'NONE',  ( 52.99265158129170317, 95.25000000000000000, 346.9005000000000223 ) ) ;
#83318=DIRECTION ( 'NONE',  ( 0.000000000000000000, 0.000000000000000000, 1.000000000000000000 ) ) ;
#83399=DIRECTION ( 'NONE',  ( 0.000000000000000000, 0.000000000000000000, 1.000000000000000000 ) ) ;
#83414=PLANE ( 'NONE',  #60175 ) ;
#83451=COLOUR_RGB ( '', 0.66274510, 0.83137255, 0.94901961) ;
#83475=VECTOR ( 'NONE', #26101, 1000.000000000000000 ) ;
#83489=DIRECTION ( 'NONE',  ( 0.000000000000000000, 1.000000000000000000, 0.000000000000000000 ) ) ;
#83521=VECTOR ( 'NONE', #19341, 1000.000000000000000 ) ;
#83531=DIRECTION ( 'NONE',  ( 0.000000000000000000, 0.000000000000000000, -1.000000000000000000 ) ) ;
#83552=LINE ( 'NONE', #63544, #86465 ) ;
#83592=CARTESIAN_POINT ( 'NONE',  ( 6.938893903907229955E-15, 60.82030000000000314, 216.0269999999999868 ) ) ;
#83610=AXIS2_PLACEMENT_3D ( 'NONE', #20289, #13463, #13024 ) ;
#83649=CYLINDRICAL_SURFACE ( 'NONE', #30541, 3.174999999999983391 ) ;
#83674=AXIS2_PLACEMENT_3D ( 'NONE', #35507, #21003, #84592 ) ;
#83699=LINE ( 'NONE', #29179, #86332 ) ;
#83722=CIRCLE ( 'NONE', #9743, 16.09746158385918946 ) ;
#83905=CIRCLE ( 'NONE', #34530, 16.09746158385918946 ) ;
#83953=CARTESIAN_POINT ( 'NONE',  ( 12.27414673259628586, 85.42709173517430088, 117.9189431488524917 ) ) ;
#83963=ORIENTED_EDGE ( 'NONE', *, *, #53119, .F. ) ;
#83967=PLANE ( 'NONE',  #35458 ) ;
#84048=DIRECTION ( 'NONE',  ( 0.000000000000000000, 0.000000000000000000, 1.000000000000000000 ) ) ;
#84073=EDGE_LOOP ( 'NONE', ( #59976, #84470, #81060 ) ) ;
#84096=ADVANCED_FACE ( 'NONE', ( #8702 ), #64993, .F. ) ;
#84149=EDGE_CURVE ( 'NONE', #46574, #56872, #79532, .T. ) ;
#84178=FACE_OUTER_BOUND ( 'NONE', #54913, .T. ) ;
#84191=UNCERTAINTY_MEASURE_WITH_UNIT (LENGTH_MEASURE( 1.000000000000000082E-05 ), #19161, 'distance_accuracy_value', 'NONE');
#84197=DIRECTION ( 'NONE',  ( -0.000000000000000000, -0.000000000000000000, 1.000000000000000000 ) ) ;
#84199=CARTESIAN_POINT ( 'NONE',  ( 38.10000000000000142, 95.25000000000000000, 283.4005000000000223 ) ) ;
#84285=ORIENTED_EDGE ( 'NONE', *, *, #57123, .T. ) ;
#84351=ORIENTED_EDGE ( 'NONE', *, *, #72446, .T. ) ;
#84470=ORIENTED_EDGE ( 'NONE', *, *, #76617, .T. ) ;
#84473=DIRECTION ( 'NONE',  ( 0.000000000000000000, 1.000000000000000000, 0.000000000000000000 ) ) ;
#84490=CARTESIAN_POINT ( 'NONE',  ( 23.49602674866495988, 79.64193718108693076, 299.1106646571903411 ) ) ;
#84581=CARTESIAN_POINT ( 'NONE',  ( 23.75871628398702384, 82.86657936785965717, 298.1325000000000500 ) ) ;
#84592=DIRECTION ( 'NONE',  ( 0.000000000000000000, 0.000000000000000000, 1.000000000000000000 ) ) ;
#84595=DIRECTION ( 'NONE',  ( 0.000000000000000000, 0.000000000000000000, -1.000000000000000000 ) ) ;
#84598=VERTEX_POINT ( 'NONE', #16742 ) ;
#84628=DIRECTION ( 'NONE',  ( 0.000000000000000000, 0.000000000000000000, 1.000000000000000000 ) ) ;
#84637=DIRECTION ( 'NONE',  ( 0.000000000000000000, -1.000000000000000000, 0.000000000000000000 ) ) ;
#84708=CARTESIAN_POINT ( 'NONE',  ( 69.25310000000000343, 82.54999999999999716, 344.4418053999999643 ) ) ;
#84734=ORIENTED_EDGE ( 'NONE', *, *, #45147, .T. ) ;
#84765=LINE ( 'NONE', #22094, #200 ) ;
#84772=DIRECTION ( 'NONE',  ( -1.092739197465703932E-16, 1.000000000000000000, 0.000000000000000000 ) ) ;
#84796=VECTOR ( 'NONE', #89611, 1000.000000000000000 ) ;
#84833=EDGE_LOOP ( 'NONE', ( #14330, #8584, #22365, #19049 ) ) ;
#84842=EDGE_CURVE ( 'NONE', #27014, #7823, #52827, .T. ) ;
#84852=CARTESIAN_POINT ( 'NONE',  ( 7.336227921918954564, 92.80226562212374120, 118.3292963051747932 ) ) ;
#84917=AXIS2_PLACEMENT_3D ( 'NONE', #80308, #60275, #3987 ) ;
#85001=CARTESIAN_POINT ( 'NONE',  ( 38.10000000000000142, 95.25000000000000000, 283.4005000000000223 ) ) ;
#85004=LINE ( 'NONE', #37733, #55214 ) ;
#85012=CARTESIAN_POINT ( 'NONE',  ( 44.45000000000000284, 50.79999999999999716, 257.1750000000000114 ) ) ;
#85065=VERTEX_POINT ( 'NONE', #52374 ) ;
#85144=CARTESIAN_POINT ( 'NONE',  ( 2.861368367625729547, 70.27219044652896685, 118.5221636901931817 ) ) ;
#85158=VERTEX_POINT ( 'NONE', #60553 ) ;
#85183=EDGE_CURVE ( 'NONE', #51227, #45628, #4268, .T. ) ;
#85284=EDGE_CURVE ( 'NONE', #28761, #40995, #33312, .T. ) ;
#85303=EDGE_LOOP ( 'NONE', ( #26545, #40827, #23521, #14124 ) ) ;
#85394=EDGE_LOOP ( 'NONE', ( #29739, #37360, #45071, #38842 ) ) ;
#85450=FACE_OUTER_BOUND ( 'NONE', #52860, .T. ) ;
#85494=DIRECTION ( 'NONE',  ( 0.000000000000000000, -1.000000000000000000, 0.000000000000000000 ) ) ;
#85513=DIRECTION ( 'NONE',  ( 0.000000000000000000, 1.000000000000000000, 0.000000000000000000 ) ) ;
#85591=CARTESIAN_POINT ( 'NONE',  ( 11.93751238659888614, 78.49696472779160672, 117.9535311651797684 ) ) ;
#85667=LINE ( 'NONE', #57031, #55892 ) ;
#85819=VERTEX_POINT ( 'NONE', #69077 ) ;
#85836=ORIENTED_EDGE ( 'NONE', *, *, #27922, .F. ) ;
#85876=EDGE_LOOP ( 'NONE', ( #9579, #79165, #76989, #34010 ) ) ;
#85909=EDGE_CURVE ( 'NONE', #27014, #8926, #63383, .T. ) ;
#85946=VECTOR ( 'NONE', #87974, 1000.000000000000000 ) ;
#86004=EDGE_CURVE ( 'NONE', #20045, #17829, #79485, .T. ) ;
#86020=ORIENTED_EDGE ( 'NONE', *, *, #14395, .F. ) ;
#86093=DIRECTION ( 'NONE',  ( -0.7071067811865474617, 0.000000000000000000, -0.7071067811865474617 ) ) ;
#86110=ORIENTED_EDGE ( 'NONE', *, *, #11022, .F. ) ;
#86128=CYLINDRICAL_SURFACE ( 'NONE', #20243, 4.762500000000002842 ) ;
#86148=LINE ( 'NONE', #66122, #87387 ) ;
#86161=VERTEX_POINT ( 'NONE', #44479 ) ;
#86208=AXIS2_PLACEMENT_3D ( 'NONE', #34393, #28477, #55707 ) ;
#86210=AXIS2_PLACEMENT_3D ( 'NONE', #70771, #8996, #8089 ) ;
#86245=VERTEX_POINT ( 'NONE', #19920 ) ;
#86282=ORIENTED_EDGE ( 'NONE', *, *, #24893, .T. ) ;
#86288=EDGE_CURVE ( 'NONE', #41217, #32950, #67784, .T. ) ;
#86307=EDGE_LOOP ( 'NONE', ( #20469, #72911 ) ) ;
#86310=EDGE_CURVE ( 'NONE', #37287, #89758, #67616, .T. ) ;
#86330=ORIENTED_EDGE ( 'NONE', *, *, #23044, .F. ) ;
#86332=VECTOR ( 'NONE', #56865, 1000.000000000000000 ) ;
#86356=CARTESIAN_POINT ( 'NONE',  ( 23.22048716318218098, 86.68168211238419474, 300.5057518000332948 ) ) ;
#86360=ORIENTED_EDGE ( 'NONE', *, *, #74093, .T. ) ;
#86449=VERTEX_POINT ( 'NONE', #15802 ) ;
#86465=VECTOR ( 'NONE', #70363, 1000.000000000000000 ) ;
#86469=DIRECTION ( 'NONE',  ( 0.000000000000000000, 0.000000000000000000, 1.000000000000000000 ) ) ;
#86499=EDGE_CURVE ( 'NONE', #69509, #46472, #14171, .T. ) ;
#86523=AXIS2_PLACEMENT_3D ( 'NONE', #61367, #26416, #75008 ) ;
#86555=CARTESIAN_POINT ( 'NONE',  ( 70.58666025953209555, 82.54999999999999716, 344.4418053999999643 ) ) ;
#86595=VERTEX_POINT ( 'NONE', #38021 ) ;
#86620=ORIENTED_EDGE ( 'NONE', *, *, #2744, .F. ) ;
#86631=CARTESIAN_POINT ( 'NONE',  ( 45.66030316258350297, 82.54999999999999716, 358.0130000000000337 ) ) ;
#86682=DIRECTION ( 'NONE',  ( 1.000000000000000000, 0.000000000000000000, 0.000000000000000000 ) ) ;
#86718=DIRECTION ( 'NONE',  ( 0.000000000000000000, 1.000000000000000000, 0.000000000000000000 ) ) ;
#86722=DIRECTION ( 'NONE',  ( -1.821231995776174246E-16, 0.000000000000000000, -1.000000000000000000 ) ) ;
#86723=ADVANCED_FACE ( 'NONE', ( #19367 ), #67500, .T. ) ;
#86798=CARTESIAN_POINT ( 'NONE',  ( 23.35572197099206448, 86.13643889426903399, 306.0438936232959577 ) ) ;
#86832=DIRECTION ( 'NONE',  ( 1.000000000000000000, 0.000000000000000000, 0.000000000000000000 ) ) ;
#86834=ORIENTED_EDGE ( 'NONE', *, *, #89069, .F. ) ;
#86847=ORIENTED_EDGE ( 'NONE', *, *, #25316, .F. ) ;
#86873=DIRECTION ( 'NONE',  ( -1.000000000000000000, 0.000000000000000000, -1.092739197465703932E-16 ) ) ;
#86880=AXIS2_PLACEMENT_3D ( 'NONE', #40963, #27786, #20983 ) ;
#86893=AXIS2_PLACEMENT_3D ( 'NONE', #67294, #11902, #25519 ) ;
#86917=EDGE_LOOP ( 'NONE', ( #39894, #8602, #86330, #79235 ) ) ;
#86923=DIRECTION ( 'NONE',  ( -1.000000000000000000, 0.000000000000000000, 0.000000000000000000 ) ) ;
#86935=DIRECTION ( 'NONE',  ( 0.000000000000000000, -0.5150380749100549327, -0.8571673007021118895 ) ) ;
#86936=CARTESIAN_POINT ( 'NONE',  ( 8.398627748552550652E-16, 50.79999999999999716, 272.4150000000000205 ) ) ;
#86943=CIRCLE ( 'NONE', #66636, 5.562599999999973122 ) ;
#87037=ORIENTED_EDGE ( 'NONE', *, *, #56319, .T. ) ;
#87078=DIRECTION ( 'NONE',  ( 0.000000000000000000, 0.000000000000000000, 1.000000000000000000 ) ) ;
#87086=VECTOR ( 'NONE', #18982, 1000.000000000000000 ) ;
#87142=DIRECTION ( 'NONE',  ( 0.000000000000000000, 0.000000000000000000, 1.000000000000000000 ) ) ;
#87154=FACE_OUTER_BOUND ( 'NONE', #30040, .T. ) ;
#87199=DIRECTION ( 'NONE',  ( 0.000000000000000000, 1.000000000000000000, 0.000000000000000000 ) ) ;
#87212=PLANE ( 'NONE',  #61576 ) ;
#87288=EDGE_CURVE ( 'NONE', #52932, #82905, #49970, .T. ) ;
#87312=CARTESIAN_POINT ( 'NONE',  ( 28.57499999999999929, 91.71543552338529537, 302.8950000000000387 ) ) ;
#87322=CARTESIAN_POINT ( 'NONE',  ( 31.75000000000000000, 66.67499999999999716, 295.2750000000000341 ) ) ;
#87335=DIRECTION ( 'NONE',  ( 1.000000000000000000, 0.000000000000000000, 0.000000000000000000 ) ) ;
#87379=DIRECTION ( 'NONE',  ( 4.649954031768962643E-17, 0.8660254037844382635, 0.5000000000000008882 ) ) ;
#87387=VECTOR ( 'NONE', #31160, 1000.000000000000000 ) ;
#87449=EDGE_CURVE ( 'NONE', #47202, #35448, #79543, .T. ) ;
#87469=EDGE_LOOP ( 'NONE', ( #40722, #33992, #38754, #41108, #14789, #67955 ) ) ;
#87549=ORIENTED_EDGE ( 'NONE', *, *, #15758, .F. ) ;
#87576=EDGE_CURVE ( 'NONE', #86245, #65225, #34450, .T. ) ;
#87616=AXIS2_PLACEMENT_3D ( 'NONE', #25800, #66683, #3566 ) ;
#87635=CARTESIAN_POINT ( 'NONE',  ( 28.57499999999999929, 77.96728223830730542, 294.9574999999999818 ) ) ;
#87653=LINE ( 'NONE', #52642, #87792 ) ;
#87655=ORIENTED_EDGE ( 'NONE', *, *, #9393, .F. ) ;
#87689=ORIENTED_EDGE ( 'NONE', *, *, #78516, .F. ) ;
#87748=VECTOR ( 'NONE', #73577, 1000.000000000000000 ) ;
#87757=LINE ( 'NONE', #11906, #78925 ) ;
#87792=VECTOR ( 'NONE', #74017, 1000.000000000000000 ) ;
#87819=EDGE_LOOP ( 'NONE', ( #54462, #73280, #83963, #3376 ) ) ;
#87896=DIRECTION ( 'NONE',  ( 0.000000000000000000, -1.000000000000000000, 0.000000000000000000 ) ) ;
#87920=CARTESIAN_POINT ( 'NONE',  ( 57.14999999999999858, 95.25000000000000000, 280.2255000000000109 ) ) ;
#87974=DIRECTION ( 'NONE',  ( -1.092739197465703932E-16, 0.000000000000000000, 1.000000000000000000 ) ) ;
#88031=DIRECTION ( 'NONE',  ( 0.000000000000000000, -1.000000000000000000, 0.000000000000000000 ) ) ;
#88091=B_SPLINE_CURVE_WITH_KNOTS ( 'NONE', 3,
 ( #27797, #84581, #75956, #22341, #15531, #43204, #62315, #99, #64123, #23256, #44990, #86356, #71395, #37756, #72279, #1893, #29592, #31368, #52233, #58189, #79549, #57741, #71830, #2345, #8721, #24126, #86798, #51798, #65454, #17311, #64566, #78669, #10049, #72720, #16419, #30048, #57283, #79996 ),
 .UNSPECIFIED., .F., .F.,
 ( 4, 2, 2, 2, 2, 2, 2, 2, 2, 2, 2, 2, 2, 2, 2, 2, 2, 2, 4 ),
 ( 0.000000000000000000, 0.0009358755680944266103, 0.001871751136188853221, 0.002807626704283279831, 0.003743502272377706441, 0.004679377840472133052, 0.005615253408566559662, 0.006083191192613696639, 0.006551128976660833617, 0.007487004544755115377, 0.008422880112849397138, 0.009358755680943678032, 0.01029463124903796066, 0.01123050681713224155, 0.01216638238522652592, 0.01310225795332080681, 0.01403813352141508944, 0.01450607130546224983, 0.01497400908950941197 ),
 .UNSPECIFIED. ) ;
#88103=CIRCLE ( 'NONE', #48896, 3.174999999999983391 ) ;
#88125=EDGE_CURVE ( 'NONE', #1395, #62569, #74349, .T. ) ;
#88127=DIRECTION ( 'NONE',  ( 0.000000000000000000, 0.000000000000000000, -1.000000000000000000 ) ) ;
#88163=CARTESIAN_POINT ( 'NONE',  ( 23.03808826316528169, 77.78751545737644335, 303.0524246975253959 ) ) ;
#88184=EDGE_CURVE ( 'NONE', #68410, #75721, #17222, .T. ) ;
#88196=PLANE ( 'NONE',  #41342 ) ;
#88209=CARTESIAN_POINT ( 'NONE',  ( -10.01853500445675671, 74.86481845265393531, 118.1328220722729441 ) ) ;
#88240=CIRCLE ( 'NONE', #47616, 13.09746158385919124 ) ;
#88286=CARTESIAN_POINT ( 'NONE',  ( -6.314145302152993189, 93.48478343411423452, 118.3897254880733669 ) ) ;
#88288=FACE_OUTER_BOUND ( 'NONE', #40295, .T. ) ;
#88313=VECTOR ( 'NONE', #86682, 1000.000000000000000 ) ;
#88326=LINE ( 'NONE', #32426, #13433 ) ;
#88344=CIRCLE ( 'NONE', #59267, 10.26166025953211758 ) ;
#88418=CARTESIAN_POINT ( 'NONE',  ( -7.661254700127833495, 82.54999999999999716, 320.6630000000000109 ) ) ;
#88608=CARTESIAN_POINT ( 'NONE',  ( 23.58193636576847751, 80.15658928983457088, 307.0240681300007282 ) ) ;
#88654=CARTESIAN_POINT ( 'NONE',  ( -12.59999999999999787, 82.13878092619209781, 117.8845415480757310 ) ) ;
#88674=ORIENTED_EDGE ( 'NONE', *, *, #35609, .F. ) ;
#88689=CARTESIAN_POINT ( 'NONE',  ( 60.32499999999999574, 82.54999999999999716, 358.0130000000000337 ) ) ;
#88782=CARTESIAN_POINT ( 'NONE',  ( -44.45000000000000284, 114.2999999999999972, 275.4630000000000223 ) ) ;
#88791=ORIENTED_EDGE ( 'NONE', *, *, #73461, .T. ) ;
#88843=ORIENTED_EDGE ( 'NONE', *, *, #10443, .T. ) ;
#88845=AXIS2_PLACEMENT_3D ( 'NONE', #584, #82839, #28284 ) ;
#88924=DIRECTION ( 'NONE',  ( 0.000000000000000000, 1.000000000000000000, 0.000000000000000000 ) ) ;
#88989=CARTESIAN_POINT ( 'NONE',  ( 0.000000000000000000, 65.60000000000000853, 0.000000000000000000 ) ) ;
#89069=EDGE_CURVE ( 'NONE', #40033, #14287, #52154, .T. ) ;
#89072=VERTEX_POINT ( 'NONE', #45350 ) ;
#89102=CARTESIAN_POINT ( 'NONE',  ( 47.62500000000000000, 73.02500000000000568, 257.1750000000000114 ) ) ;
#89117=LINE ( 'NONE', #26876, #72672 ) ;
#89137=ORIENTED_EDGE ( 'NONE', *, *, #14200, .T. ) ;
#89144=DIRECTION ( 'NONE',  ( -9.299908063537909262E-17, 6.056575390184510167E-15, -1.000000000000000000 ) ) ;
#89263=VERTEX_POINT ( 'NONE', #7953 ) ;
#89324=CARTESIAN_POINT ( 'NONE',  ( 34.92499999999999716, 69.84999999999999432, 295.2750000000000341 ) ) ;
#89381=DIRECTION ( 'NONE',  ( -1.000000000000000000, 0.000000000000000000, 1.821231995776179916E-16 ) ) ;
#89387=EDGE_LOOP ( 'NONE', ( #43605, #75866, #60078, #39826, #16906, #67496, #31820, #25249, #21208, #23825, #80649, #20926, #18681 ) ) ;
#89413=CARTESIAN_POINT ( 'NONE',  ( 47.62500000000000000, 94.53880000000000905, 225.4249999999999829 ) ) ;
#89446=AXIS2_PLACEMENT_3D ( 'NONE', #56728, #84473, #22237 ) ;
#89460=ORIENTED_EDGE ( 'NONE', *, *, #21714, .F. ) ;
#89507=DIRECTION ( 'NONE',  ( 9.299908063537919123E-17, 0.000000000000000000, 1.000000000000000000 ) ) ;
#89508=VECTOR ( 'NONE', #89381, 1000.000000000000000 ) ;
#89545=CARTESIAN_POINT ( 'NONE',  ( -12.49830498548568158, 80.89921386390227553, 117.8953739236498990 ) ) ;
#89549=ORIENTED_EDGE ( 'NONE', *, *, #44765, .T. ) ;
#89581=ADVANCED_FACE ( 'NONE', ( #32659, #24959, #38577 ), #81734, .F. ) ;
#89587=ORIENTED_EDGE ( 'NONE', *, *, #85909, .F. ) ;
#89611=DIRECTION ( 'NONE',  ( 0.000000000000000000, 1.000000000000000000, 0.000000000000000000 ) ) ;
#89656=CARTESIAN_POINT ( 'NONE',  ( 0.000000000000000000, 0.000000000000000000, 0.000000000000000000 ) ) ;
#89676=VECTOR ( 'NONE', #67806, 1000.000000000000000 ) ;
#89735=EDGE_LOOP ( 'NONE', ( #3978, #25474, #25769, #51402, #87655, #64584 ) ) ;
#89745=ORIENTED_EDGE ( 'NONE', *, *, #68550, .F. ) ;
#89758=VERTEX_POINT ( 'NONE', #71234 ) ;
ENDSEC;
END-ISO-10303-21;
